ISO-10303-21;
HEADER;
FILE_DESCRIPTION (('STEP AP214'),
    '1' );
FILE_NAME ('hex flange nut gradea_iso_ISO - 4161 - M5 - N.step',
    '2026-10-25T07:12:54',
    ( '' ),
    ( '' ),
    'SwSTEP 2.0',
    'SolidWorks 2026',
    '' );
FILE_SCHEMA (( 'AUTOMOTIVE_DESIGN' ));
ENDSEC;

DATA;
#11=ORIENTED_EDGE ( 'NONE', *, *, #3487, .F. ) ;
#16=CARTESIAN_POINT ( 'NONE',  ( -2.100000000000000089, 2.571758278209441957E-16, -4.694516984716113228 ) ) ;
#41=CARTESIAN_POINT ( 'NONE',  ( -1.360585162435467455, 4.061296242128285883, -3.505054077164959203 ) ) ;
#54=CARTESIAN_POINT ( 'NONE',  ( 3.861362476283255685, 2.629030857715988656, -3.671615880910370500 ) ) ;
#89=CARTESIAN_POINT ( 'NONE',  ( 4.000000000000000888, 1.539600717838996990, -3.300726591567079815 ) ) ;
#99=EDGE_CURVE ( 'NONE', #9288, #2470, #13475, .T. ) ;
#119=CARTESIAN_POINT ( 'NONE',  ( -1.287237434361707233, -3.875615274277397937, -3.430618716626816500 ) ) ;
#122=CARTESIAN_POINT ( 'NONE',  ( 0.000000000000000000, 0.000000000000000000, 0.000000000000000000 ) ) ;
#123=CARTESIAN_POINT ( 'NONE',  ( -3.355112389629170799, 2.681727112203152963, -0.2256878752776689534 ) ) ;
#124=CARTESIAN_POINT ( 'NONE',  ( 4.024499207728657879, 2.323545700935571556, -3.572172305156506411 ) ) ;
#133=EDGE_LOOP ( 'NONE', ( #295, #3127 ) ) ;
#169=CARTESIAN_POINT ( 'NONE',  ( -4.000000000000000000, -0.7890432684750890990, -0.04868663549882315533 ) ) ;
#180=SHAPE_REPRESENTATION ( 'hex flange nut gradea_iso_ISO - 4161 - M5 - N', ( #430 ), #9487 ) ;
#197=EDGE_CURVE ( 'NONE', #1117, #3434, #12820, .T. ) ;
#204=CARTESIAN_POINT ( 'NONE',  ( 8.673617379884035472E-16, 4.618802153517012954, 0.000000000000000000 ) ) ;
#226=CARTESIAN_POINT ( 'NONE',  ( -4.000000000000000000, -2.309401076758512694, -5.000000000000000000 ) ) ;
#248=CARTESIAN_POINT ( 'NONE',  ( 0.1410422978106145031, -4.700232962125109104, -3.687027686973628704 ) ) ;
#249=DIRECTION ( 'NONE',  ( 0.000000000000000000, 0.000000000000000000, 1.000000000000000000 ) ) ;
#270=CARTESIAN_POINT ( 'NONE',  ( -3.333333333333335258, 2.694301256218251783, -3.300726591567079815 ) ) ;
#279=ORIENTED_EDGE ( 'NONE', *, *, #2210, .T. ) ;
#282=CARTESIAN_POINT ( 'NONE',  ( -3.679171394226034675, -2.494631558665844739, -0.3503314178412558211 ) ) ;
#284=EDGE_CURVE ( 'NONE', #3263, #6584, #5155, .T. ) ;
#286=CARTESIAN_POINT ( 'NONE',  ( 1.655952806101427033, -3.662737355149048302, -1.182683869819604841E-14 ) ) ;
#295=ORIENTED_EDGE ( 'NONE', *, *, #8457, .F. ) ;
#301=CARTESIAN_POINT ( 'NONE',  ( 2.805705207896068476, -3.226868319750173075, -3.503898532754370354 ) ) ;
#309=ORIENTED_EDGE ( 'NONE', *, *, #197, .T. ) ;
#322=TOROIDAL_SURFACE ( 'NONE', #9170, 5.384454397937118664, 0.5155456020628804703 ) ;
#330=ORIENTED_EDGE ( 'NONE', *, *, #7102, .T. ) ;
#357=DIRECTION ( 'NONE',  ( 0.000000000000000000, -0.000000000000000000, 1.000000000000000000 ) ) ;
#374=CARTESIAN_POINT ( 'NONE',  ( 4.000000000000003553, -2.309401076758513138, -3.504271511726786859 ) ) ;
#378=DIRECTION ( 'NONE',  ( 0.000000000000000000, 0.000000000000000000, -1.000000000000000000 ) ) ;
#420=CARTESIAN_POINT ( 'NONE',  ( 1.287237434362044075, 3.875615274277557809, -3.430618716626812059 ) ) ;
#422=CARTESIAN_POINT ( 'NONE',  ( -2.805705207896067144, 3.226868319750155312, -3.503898532754364581 ) ) ;
#430=AXIS2_PLACEMENT_3D ( 'NONE', #5828, #10990, #3471 ) ;
#444=CARTESIAN_POINT ( 'NONE',  ( 1.243802165048773611, -3.900692638707475624, -3.223146290109810241 ) ) ;
#475=ORIENTED_EDGE ( 'NONE', *, *, #7215, .F. ) ;
#508=DIRECTION ( 'NONE',  ( -1.000000000000000000, 0.000000000000000000, 0.000000000000000000 ) ) ;
#509=CARTESIAN_POINT ( 'NONE',  ( 3.680118525130245732, -2.494084732383344605, -0.3507732604232533524 ) ) ;
#528=CARTESIAN_POINT ( 'NONE',  ( -4.204015924366189871, 1.626724848190922446, -3.610627190413390419 ) ) ;
#537=ORIENTED_EDGE ( 'NONE', *, *, #7115, .F. ) ;
#560=ADVANCED_FACE ( 'NONE', ( #5371 ), #7377, .F. ) ;
#565=DIRECTION ( 'NONE',  ( -1.000000000000000000, 0.000000000000000000, 0.000000000000000000 ) ) ;
#566=EDGE_LOOP ( 'NONE', ( #6329, #10316, #10441 ) ) ;
#571=CARTESIAN_POINT ( 'NONE',  ( -5.560781378645573980, 0.000000000000000000, -4.000000000000000000 ) ) ;
#584=CARTESIAN_POINT ( 'NONE',  ( 4.000000000000000000, 2.309401076758497151, -5.000000000000000000 ) ) ;
#588=CYLINDRICAL_SURFACE ( 'NONE', #12577, 2.500000000000000444 ) ;
#592=CARTESIAN_POINT ( 'NONE',  ( -4.024497503033519941, 2.323544716729375459, -3.572167766733379768 ) ) ;
#596=ORIENTED_EDGE ( 'NONE', *, *, #7970, .T. ) ;
#627=CARTESIAN_POINT ( 'NONE',  ( -4.000000000000000000, 2.309401076758498483, -5.000000000000000000 ) ) ;
#658=DIRECTION ( 'NONE',  ( 1.000000000000000000, 0.000000000000000000, 0.000000000000000000 ) ) ;
#661=DIRECTION ( 'NONE',  ( 1.000000000000000000, 0.000000000000000000, 0.000000000000000000 ) ) ;
#671=CARTESIAN_POINT ( 'NONE',  ( -0.6920835326022555245, -4.454600218803899558, -3.597382984111586079 ) ) ;
#680=DIRECTION ( 'NONE',  ( 0.9396926207859138680, 1.150791560227856926E-16, -0.3420201433256536139 ) ) ;
#687=EDGE_CURVE ( 'NONE', #7344, #3771, #10007, .T. ) ;
#688=CARTESIAN_POINT ( 'NONE',  ( -1.747541505913277282, 3.837784562140256650, -3.503702292528906526 ) ) ;
#691=ORIENTED_EDGE ( 'NONE', *, *, #12541, .F. ) ;
#695=CIRCLE ( 'NONE', #1587, 4.000000000000000000 ) ;
#700=DIRECTION ( 'NONE',  ( 0.000000000000000000, -0.000000000000000000, 1.000000000000000000 ) ) ;
#730=DIRECTION ( 'NONE',  ( 0.000000000000000000, 0.000000000000000000, 1.000000000000000000 ) ) ;
#732=CARTESIAN_POINT ( 'NONE',  ( 4.000000000000000000, -0.8732470631449981147, -3.223155494240760088 ) ) ;
#741=ORIENTED_EDGE ( 'NONE', *, *, #6618, .T. ) ;
#755=CARTESIAN_POINT ( 'NONE',  ( -4.000000000000000000, 0.8576368993457507139, -3.433240632782198709 ) ) ;
#763=B_SPLINE_CURVE_WITH_KNOTS ( 'NONE', 3,
 ( #5749, #11051, #9056, #592, #12230, #1570 ),
 .UNSPECIFIED., .F., .F.,
 ( 4, 2, 4 ),
 ( -3.640115492410698714E-06, 0.0002066546034006521879, 0.0004169493222937151081 ),
 .UNSPECIFIED. ) ;
#805=CARTESIAN_POINT ( 'NONE',  ( -4.203833317240879275, -1.627343821129593859, -3.597273115243890818 ) ) ;
#808=ORIENTED_EDGE ( 'NONE', *, *, #8589, .F. ) ;
#818=CARTESIAN_POINT ( 'NONE',  ( -4.197312064133472020, -0.8182229787990021874, -3.502518405183886685 ) ) ;
#820=AXIS2_PLACEMENT_3D ( 'NONE', #10787, #8864, #7690 ) ;
#832=EDGE_CURVE ( 'NONE', #7686, #1117, #3261, .T. ) ;
#840=EDGE_CURVE ( 'NONE', #3920, #7551, #3094, .T. ) ;
#847=CARTESIAN_POINT ( 'NONE',  ( -4.000000000000000000, 2.309401076758498483, -5.000000000000000000 ) ) ;
#857=CARTESIAN_POINT ( 'NONE',  ( -3.522875095019672109, 2.820352903225427532, -3.598441714920591394 ) ) ;
#860=LINE ( 'NONE', #12748, #12328 ) ;
#868=ORIENTED_EDGE ( 'NONE', *, *, #8531, .T. ) ;
#883=EDGE_CURVE ( 'NONE', #13411, #7551, #2265, .T. ) ;
#900=CARTESIAN_POINT ( 'NONE',  ( -6.473970235329672780E-16, -4.862606272033106691, -3.745885042887442395 ) ) ;
#909=VECTOR ( 'NONE', #1619, 1000.000000000000000 ) ;
#914=CARTESIAN_POINT ( 'NONE',  ( 0.000000000000000000, 0.000000000000000000, -4.974599999999998801 ) ) ;
#923=EDGE_LOOP ( 'NONE', ( #4335, #13115, #1965, #9708, #10853 ) ) ;
#924=CARTESIAN_POINT ( 'NONE',  ( 2.000000000000000444, 3.464101615137754830, -3.142992957459231018 ) ) ;
#928=EDGE_CURVE ( 'NONE', #6427, #7344, #12002, .T. ) ;
#952=DIRECTION ( 'NONE',  ( -1.000000000000000000, 0.000000000000000000, 0.000000000000000000 ) ) ;
#954=CARTESIAN_POINT ( 'NONE',  ( 4.197393957002303999, 0.8151795401431359833, -3.503767560748935139 ) ) ;
#968=PRODUCT_DEFINITION_CONTEXT ( 'detailed design', #5938, 'design' ) ;
#969=EDGE_LOOP ( 'NONE', ( #7359, #2872, #11647, #5301 ) ) ;
#989=CARTESIAN_POINT ( 'NONE',  ( 2.100000000000000089, 0.000000000000000000, -5.000000000000000000 ) ) ;
#1002=EDGE_LOOP ( 'NONE', ( #6522, #6191, #11931, #5858 ) ) ;
#1006=CARTESIAN_POINT ( 'NONE',  ( 0.000000000000000000, 0.000000000000000000, -5.000000000000000000 ) ) ;
#1023=DIRECTION ( 'NONE',  ( 1.000000000000000000, 0.000000000000000000, 0.000000000000000000 ) ) ;
#1059=CARTESIAN_POINT ( 'NONE',  ( -0.5469614295416921346, 4.303013824936271270, -3.535263753543735454 ) ) ;
#1068=CARTESIAN_POINT ( 'NONE',  ( -0.5449313310646672903, -4.304185902836978883, -3.316620875263469159 ) ) ;
#1105=CARTESIAN_POINT ( 'NONE',  ( -4.101948962585905356, -2.368261337751088824, -3.681124513963624167 ) ) ;
#1116=EDGE_CURVE ( 'NONE', #8295, #7686, #2292, .T. ) ;
#1117=VERTEX_POINT ( 'NONE', #6728 ) ;
#1122=CIRCLE ( 'NONE', #13047, 5.560781378645573980 ) ;
#1130=DIRECTION ( 'NONE',  ( 0.8191520442889875797, 0.000000000000000000, 0.5735764363510522656 ) ) ;
#1137=CONICAL_SURFACE ( 'NONE', #8884, 2.059999999999998721, 0.9599310885968738161 ) ;
#1138=B_SPLINE_CURVE_WITH_KNOTS ( 'NONE', 3,
 ( #9599, #1271, #123, #10701, #2058, #12700, #3371, #7460 ),
 .UNSPECIFIED., .F., .F.,
 ( 4, 2, 2, 4 ),
 ( 2.465131517071352357E-07, 0.001183067374689843057, 0.001774477805458910071, 0.002365888236227977302 ),
 .UNSPECIFIED. ) ;
#1194=CARTESIAN_POINT ( 'NONE',  ( -4.000000000000000000, 0.000000000000000000, 0.000000000000000000 ) ) ;
#1213=CARTESIAN_POINT ( 'NONE',  ( 2.449848172108560096, 3.432307619358740514, -3.503702292528905637 ) ) ;
#1243=DIRECTION ( 'NONE',  ( 1.000000000000000000, 0.000000000000000000, 0.000000000000000000 ) ) ;
#1258=DIRECTION ( 'NONE',  ( 1.000000000000000000, 0.000000000000000000, 0.000000000000000000 ) ) ;
#1259=CARTESIAN_POINT ( 'NONE',  ( 3.349226789952652439, 2.685125164760731487, -0.2236248678334773199 ) ) ;
#1267=AXIS2_PLACEMENT_3D ( 'NONE', #2661, #378, #508 ) ;
#1269=CARTESIAN_POINT ( 'NONE',  ( -4.175002511812151873, -2.208363329454905877, -3.469254087858246738 ) ) ;
#1271=CARTESIAN_POINT ( 'NONE',  ( -3.680118525130244400, 2.494084732383327285, -0.3507732604232449702 ) ) ;
#1304=VERTEX_POINT ( 'NONE', #3947 ) ;
#1318=ORIENTED_EDGE ( 'NONE', *, *, #928, .T. ) ;
#1333=CARTESIAN_POINT ( 'NONE',  ( 4.211140560182196957, -2.431303136016555122, -3.745885042887436622 ) ) ;
#1336=ORIENTED_EDGE ( 'NONE', *, *, #4161, .T. ) ;
#1338=ADVANCED_FACE ( 'NONE', ( #2777 ), #4067, .F. ) ;
#1343=CARTESIAN_POINT ( 'NONE',  ( 4.211140560182196957, 2.431303136016536470, -3.745885042887433514 ) ) ;
#1358=ORIENTED_EDGE ( 'NONE', *, *, #8589, .T. ) ;
#1370=ORIENTED_EDGE ( 'NONE', *, *, #840, .F. ) ;
#1397=( NAMED_UNIT ( * ) SI_UNIT ( $, .STERADIAN. ) SOLID_ANGLE_UNIT ( ) );
#1409=CARTESIAN_POINT ( 'NONE',  ( 1.360585162435110629, -4.061296242128317857, -3.505054077164905024 ) ) ;
#1424=ORIENTED_EDGE ( 'NONE', *, *, #9057, .T. ) ;
#1435=EDGE_CURVE ( 'NONE', #5823, #6584, #2129, .T. ) ;
#1437=CIRCLE ( 'NONE', #7657, 2.500000000000000444 ) ;
#1441=VECTOR ( 'NONE', #2350, 1000.000000000000000 ) ;
#1470=CARTESIAN_POINT ( 'NONE',  ( -2.000000000000006661, 3.464101615137750834, 0.000000000000000000 ) ) ;
#1472=UNCERTAINTY_MEASURE_WITH_UNIT (LENGTH_MEASURE( 1.000000000000000082E-05 ), #7653, 'distance_accuracy_value', 'NONE');
#1490=CARTESIAN_POINT ( 'NONE',  ( -4.000000000000000000, -2.309401076758512694, -3.433295621305382461 ) ) ;
#1493=( BOUNDED_SURFACE ( )  B_SPLINE_SURFACE ( 3, 2, ( 
 ( #12623, #9246, #10548 ),
 ( #4196, #1059, #9315 ),
 ( #5311, #6150, #41 ),
 ( #13438, #4266, #5178 ),
 ( #12486, #8483, #857 ),
 ( #9388, #3021, #12686 ) ),
 .UNSPECIFIED., .F., .F., .F. ) 
 B_SPLINE_SURFACE_WITH_KNOTS ( ( 4, 2, 4 ),
 ( 3, 3 ),
 ( 0.02032853247518125531, 0.02278863295364820865, 0.02524873343211516200 ),
 ( 0.000000000000000000, 1.000000000000000000 ),
 .UNSPECIFIED. ) 
 GEOMETRIC_REPRESENTATION_ITEM ( )  RATIONAL_B_SPLINE_SURFACE ( (
 ( 1.000000000000000000, 0.8047781615896836271, 1.000000000000000000),
 ( 1.000000000000000000, 0.8123767586289967202, 1.000000000000000000),
 ( 1.000000000000000000, 0.8190662415563443322, 1.000000000000000000),
 ( 1.000000000000000000, 0.8192361015669982205, 1.000000000000000000),
 ( 1.000000000000000000, 0.8126135807103181952, 1.000000000000000000),
 ( 1.000000000000000000, 0.8047712338318587788, 1.000000000000000000) ) ) 
 REPRESENTATION_ITEM ( '' )  SURFACE ( )  );
#1502=VECTOR ( 'NONE', #9309, 1000.000000000000000 ) ;
#1527=CARTESIAN_POINT ( 'NONE',  ( -1.828356344711647319, -3.563200125723192002, -1.076197711133951296E-14 ) ) ;
#1537=PLANE ( 'NONE',  #6404 ) ;
#1543=PLANE ( 'NONE',  #1267 ) ;
#1567=CARTESIAN_POINT ( 'NONE',  ( 3.999999999999998224, 2.472263674411418588, -3.687027874309861897 ) ) ;
#1570=CARTESIAN_POINT ( 'NONE',  ( -4.000000000000000000, 2.309401076758498483, -3.433295621305379353 ) ) ;
#1580=B_SPLINE_CURVE_WITH_KNOTS ( 'NONE', 3,
 ( #7396, #3438, #2322, #1213, #2386, #4405, #54, #8627 ),
 .UNSPECIFIED., .F., .F.,
 ( 4, 2, 2, 4 ),
 ( 7.780516681398759253E-20, 0.002450665683189819696, 0.003675998524784729327, 0.004901331366379639391 ),
 .UNSPECIFIED. ) ;
#1587=AXIS2_PLACEMENT_3D ( 'NONE', #2411, #5477, #10718 ) ;
#1593=CARTESIAN_POINT ( 'NONE',  ( 1.734723475976807094E-15, 4.618802153517012954, -0.4999999999999995559 ) ) ;
#1596=AXIS2_PLACEMENT_3D ( 'NONE', #10297, #1999, #9268 ) ;
#1619=DIRECTION ( 'NONE',  ( -0.000000000000000000, -0.000000000000000000, 1.000000000000000000 ) ) ;
#1629=ORIENTED_EDGE ( 'NONE', *, *, #284, .F. ) ;
#1635=LINE ( 'NONE', #584, #5083 ) ;
#1653=CARTESIAN_POINT ( 'NONE',  ( 3.333333333333335702, -2.694301256218268215, -3.300726591567084256 ) ) ;
#1658=CARTESIAN_POINT ( 'NONE',  ( 5.560781378645573980, 6.809993116116507654E-16, -4.000000000000000000 ) ) ;
#1751=DIRECTION ( 'NONE',  ( 1.000000000000000000, 0.000000000000000000, 0.000000000000000000 ) ) ;
#1760=B_SPLINE_CURVE_WITH_KNOTS ( 'NONE', 3,
 ( #5999, #12480, #924, #13578, #8348 ),
 .UNSPECIFIED., .F., .F.,
 ( 4, 1, 4 ),
 ( 0.000000000000000000, 0.002309401076758505356, 0.004618802153517010713 ),
 .UNSPECIFIED. ) ;
#1770=CIRCLE ( 'NONE', #5116, 4.000000000000000000 ) ;
#1869=CARTESIAN_POINT ( 'NONE',  ( 1.390230914382191596, 4.043987460488659202, -3.502507215260488582 ) ) ;
#1875=EDGE_CURVE ( 'NONE', #5652, #1304, #11701, .T. ) ;
#1889=CARTESIAN_POINT ( 'NONE',  ( -4.000000000000000000, -2.309401076758512694, -3.433295621305382461 ) ) ;
#1909=CARTESIAN_POINT ( 'NONE',  ( -4.000000000000000000, -2.309401076758512694, -5.000000000000000000 ) ) ;
#1922=CARTESIAN_POINT ( 'NONE',  ( -4.000000000000000000, 0.9868501483902560878, -0.09357334158579519445 ) ) ;
#1933=CARTESIAN_POINT ( 'NONE',  ( -1.317756351988340180, 3.857995168970202116, -0.04852650426601388955 ) ) ;
#1934=CARTESIAN_POINT ( 'NONE',  ( -0.02511973781850462134, 4.877415612947412882, -3.751298745799839462 ) ) ;
#1965=ORIENTED_EDGE ( 'NONE', *, *, #2820, .T. ) ;
#1990=CARTESIAN_POINT ( 'NONE',  ( -0.6666666666666666297, -4.233901974057276973, -3.300726591567087365 ) ) ;
#1999=DIRECTION ( 'NONE',  ( 0.000000000000000000, 0.000000000000000000, 1.000000000000000000 ) ) ;
#2002=ORIENTED_EDGE ( 'NONE', *, *, #8419, .F. ) ;
#2008=CARTESIAN_POINT ( 'NONE',  ( -0.1756481739660520902, 4.720212674038980261, -3.469390959564065291 ) ) ;
#2056=ADVANCED_FACE ( 'NONE', ( #9033 ), #8656, .F. ) ;
#2058=CARTESIAN_POINT ( 'NONE',  ( -2.687328764639638656, 3.067272167851286202, -0.05923475698270370959 ) ) ;
#2072=CARTESIAN_POINT ( 'NONE',  ( 4.140404888673277384, 2.228338276487440428, -3.686887068327033390 ) ) ;
#2077=CARTESIAN_POINT ( 'NONE',  ( -4.000000000000000000, -2.512220745329312610, -3.469390707569719901 ) ) ;
#2089=CARTESIAN_POINT ( 'NONE',  ( -4.154094228333736538, -2.398367420967545627, -3.721909803043222276 ) ) ;
#2114=ORIENTED_EDGE ( 'NONE', *, *, #2820, .F. ) ;
#2118=EDGE_CURVE ( 'NONE', #2448, #5823, #7733, .T. ) ;
#2129=CIRCLE ( 'NONE', #5675, 2.500000000000000888 ) ;
#2132=ORIENTED_EDGE ( 'NONE', *, *, #197, .F. ) ;
#2147=CARTESIAN_POINT ( 'NONE',  ( -3.264650091097280831E-13, -4.796980096169642493, -3.721999068284424617 ) ) ;
#2166=CARTESIAN_POINT ( 'NONE',  ( 1.567478505476134606E-15, 4.618802153517012066, -5.000000000000000000 ) ) ;
#2171=SURFACE_STYLE_USAGE ( .BOTH. , #11851 ) ;
#2184=CARTESIAN_POINT ( 'NONE',  ( -2.756197834950067094, -3.027510591568735254, -3.223146290109809797 ) ) ;
#2186=LINE ( 'NONE', #6431, #12253 ) ;
#2209=ORIENTED_EDGE ( 'NONE', *, *, #3320, .F. ) ;
#2210=EDGE_CURVE ( 'NONE', #10214, #2490, #3793, .T. ) ;
#2213=ORIENTED_EDGE ( 'NONE', *, *, #3661, .T. ) ;
#2216=DIRECTION ( 'NONE',  ( 1.000000000000000000, 0.000000000000000000, 0.000000000000000000 ) ) ;
#2230=ORIENTED_EDGE ( 'NONE', *, *, #7281, .T. ) ;
#2232=ORIENTED_EDGE ( 'NONE', *, *, #840, .T. ) ;
#2248=ORIENTED_EDGE ( 'NONE', *, *, #7970, .F. ) ;
#2250=CARTESIAN_POINT ( 'NONE',  ( -3.472371940586054251, -2.614027278893156669, -3.320322319202162031 ) ) ;
#2265=B_SPLINE_CURVE_WITH_KNOTS ( 'NONE', 3,
 ( #1593, #2787, #4941, #7007, #11213, #13344, #7975, #12190 ),
 .UNSPECIFIED., .F., .F.,
 ( 4, 2, 2, 4 ),
 ( 2.465131517075058656E-07, 0.001183067374689851080, 0.001774477805458923299, 0.002365888236227995517 ),
 .UNSPECIFIED. ) ;
#2275=ORIENTED_EDGE ( 'NONE', *, *, #12482, .F. ) ;
#2276=ADVANCED_FACE ( 'NONE', ( #3358 ), #1137, .F. ) ;
#2281=FACE_OUTER_BOUND ( 'NONE', #3955, .T. ) ;
#2292=B_SPLINE_CURVE_WITH_KNOTS ( 'NONE', 3,
 ( #8665, #286, #3405, #4509, #4371, #11976 ),
 .UNSPECIFIED., .F., .F.,
 ( 4, 2, 4 ),
 ( 0.002365888236227967761, 0.003551327329835077609, 0.004736766423442186590 ),
 .UNSPECIFIED. ) ;
#2307=FILL_AREA_STYLE_COLOUR ( '', #4417 ) ;
#2312=DIRECTION ( 'NONE',  ( -0.000000000000000000, -0.000000000000000000, 1.000000000000000000 ) ) ;
#2322=CARTESIAN_POINT ( 'NONE',  ( 1.391697335622810172, 4.043246145443375461, -3.503898532754365913 ) ) ;
#2348=ORIENTED_EDGE ( 'NONE', *, *, #4024, .F. ) ;
#2350=DIRECTION ( 'NONE',  ( -0.000000000000000000, -0.000000000000000000, 1.000000000000000000 ) ) ;
#2369=EDGE_CURVE ( 'NONE', #3263, #2448, #1437, .T. ) ;
#2371=DIRECTION ( 'NONE',  ( 0.000000000000000000, 0.000000000000000000, -1.000000000000000000 ) ) ;
#2386=CARTESIAN_POINT ( 'NONE',  ( 2.804994570502171047, 3.229033611042449792, -3.526374918436834704 ) ) ;
#2411=CARTESIAN_POINT ( 'NONE',  ( 0.000000000000000000, 0.000000000000000000, 0.000000000000000000 ) ) ;
#2417=ORIENTED_EDGE ( 'NONE', *, *, #9417, .T. ) ;
#2441=FACE_OUTER_BOUND ( 'NONE', #1002, .T. ) ;
#2448=VERTEX_POINT ( 'NONE', #5712 ) ;
#2454=CARTESIAN_POINT ( 'NONE',  ( -0.02448733951239248641, -4.877042772274742255, -3.751161874094027571 ) ) ;
#2462=VECTOR ( 'NONE', #680, 1000.000000000000227 ) ;
#2469=ORIENTED_EDGE ( 'NONE', *, *, #6056, .T. ) ;
#2470=VERTEX_POINT ( 'NONE', #9090 ) ;
#2472=AXIS2_PLACEMENT_3D ( 'NONE', #8031, #13399, #11132 ) ;
#2476=DIRECTION ( 'NONE',  ( 0.000000000000000000, 0.000000000000000000, -1.000000000000000000 ) ) ;
#2489=EDGE_LOOP ( 'NONE', ( #2927, #10019, #8133, #3347, #10384, #2230, #11123 ) ) ;
#2490=VERTEX_POINT ( 'NONE', #7853 ) ;
#2491=CARTESIAN_POINT ( 'NONE',  ( -2.344047193898593395, -3.265465875126480455, -1.054683074273691752E-14 ) ) ;
#2514=DIRECTION ( 'NONE',  ( 1.000000000000000000, 0.000000000000000000, 0.000000000000000000 ) ) ;
#2525=CARTESIAN_POINT ( 'NONE',  ( 4.204015924366189871, -1.626724848190933548, -3.610627190413393084 ) ) ;
#2534=CONICAL_SURFACE ( 'NONE', #13343, 4.000000000000000000, 0.8911886515913786111 ) ;
#2541=ORIENTED_EDGE ( 'NONE', *, *, #2369, .T. ) ;
#2545=DIRECTION ( 'NONE',  ( -1.000000000000000000, 0.000000000000000000, 0.000000000000000000 ) ) ;
#2547=PRODUCT_DEFINITION_SHAPE ( 'NONE', 'NONE',  #12316 ) ;
#2548=FACE_OUTER_BOUND ( 'NONE', #2785, .T. ) ;
#2576=EDGE_CURVE ( 'NONE', #12550, #2490, #4337, .T. ) ;
#2640=B_SPLINE_CURVE_WITH_KNOTS ( 'NONE', 3,
 ( #12607, #12732, #3140, #89, #7435 ),
 .UNSPECIFIED., .F., .F.,
 ( 4, 1, 4 ),
 ( 0.000000000000000000, 0.002309401076758505790, 0.004618802153517011580 ),
 .UNSPECIFIED. ) ;
#2645=CARTESIAN_POINT ( 'NONE',  ( 1.411581201560190495E-15, 4.862606272033091592, -3.745885042887436622 ) ) ;
#2651=AXIS2_PLACEMENT_3D ( 'NONE', #3676, #6529, #10727 ) ;
#2661=CARTESIAN_POINT ( 'NONE',  ( 8.673617379884035472E-16, 4.618802153517012954, -5.000000000000000000 ) ) ;
#2662=CARTESIAN_POINT ( 'NONE',  ( 3.522875095019493141, -2.820352903225631369, -3.598441714920572299 ) ) ;
#2663=B_SPLINE_CURVE_WITH_KNOTS ( 'NONE', 3,
 ( #2970, #6307, #7197, #11402, #1922, #6165, #5126, #8301 ),
 .UNSPECIFIED., .F., .F.,
 ( 4, 2, 2, 4 ),
 ( 0.005725059856848641743, 0.006314084072593626612, 0.006903108288338611481, 0.008081156719828581220 ),
 .UNSPECIFIED. ) ;
#2727=EDGE_CURVE ( 'NONE', #12550, #10183, #4779, .T. ) ;
#2758=EDGE_CURVE ( 'NONE', #2448, #3263, #12059, .T. ) ;
#2761=CARTESIAN_POINT ( 'NONE',  ( 4.211399257449709665, -2.459727064652517114, -3.751161691472417736 ) ) ;
#2775=FACE_OUTER_BOUND ( 'NONE', #3905, .T. ) ;
#2777=FACE_OUTER_BOUND ( 'NONE', #8476, .T. ) ;
#2785=EDGE_LOOP ( 'NONE', ( #2209, #2348, #6141, #5563, #1336, #1370 ) ) ;
#2787=CARTESIAN_POINT ( 'NONE',  ( 0.3198814748697593746, 4.434118497892183264, -0.3507732604232499107 ) ) ;
#2793=SHAPE_DEFINITION_REPRESENTATION ( #2547, #180 ) ;
#2805=ADVANCED_FACE ( 'NONE', ( #12934 ), #12867, .T. ) ;
#2820=EDGE_CURVE ( 'NONE', #12042, #3434, #10604, .T. ) ;
#2824=ORIENTED_EDGE ( 'NONE', *, *, #6056, .F. ) ;
#2829=CARTESIAN_POINT ( 'NONE',  ( 4.000000000000000000, -1.700175430507292473, -3.320327275037661785 ) ) ;
#2848=DIRECTION ( 'NONE',  ( -1.000000000000000000, 0.000000000000000000, 0.000000000000000000 ) ) ;
#2872=ORIENTED_EDGE ( 'NONE', *, *, #2369, .F. ) ;
#2886=ADVANCED_FACE ( 'NONE', ( #11703 ), #12669, .T. ) ;
#2925=ORIENTED_EDGE ( 'NONE', *, *, #10083, .F. ) ;
#2927=ORIENTED_EDGE ( 'NONE', *, *, #5526, .F. ) ;
#2970=CARTESIAN_POINT ( 'NONE',  ( -4.000000000000000000, 0.000000000000000000, 0.000000000000000000 ) ) ;
#2972=CARTESIAN_POINT ( 'NONE',  ( 0.000000000000000000, 0.000000000000000000, -0.2800830152838844622 ) ) ;
#2979=AXIS2_PLACEMENT_3D ( 'NONE', #4884, #11020, #1751 ) ;
#2986=DIRECTION ( 'NONE',  ( -0.000000000000000000, 0.000000000000000000, -1.000000000000000000 ) ) ;
#2991=CARTESIAN_POINT ( 'NONE',  ( -4.000000000000000000, -1.680117682357936904, -3.316611593218794951 ) ) ;
#3021=CARTESIAN_POINT ( 'NONE',  ( -4.141042297810615835, 2.227970268150415656, -3.687027686973619822 ) ) ;
#3063=CARTESIAN_POINT ( 'NONE',  ( -4.000000000000000000, -2.309401076758512694, -3.433295621305382461 ) ) ;
#3075=CARTESIAN_POINT ( 'NONE',  ( -4.000000000000000000, 2.309401076758498483, -3.433295621305379353 ) ) ;
#3094=CIRCLE ( 'NONE', #12580, 4.000000000000000000 ) ;
#3096=ORIENTED_EDGE ( 'NONE', *, *, #4024, .T. ) ;
#3115=CARTESIAN_POINT ( 'NONE',  ( 4.211140560182196957, -2.431303136016555122, -3.745885042887436622 ) ) ;
#3117=CARTESIAN_POINT ( 'NONE',  ( 2.742827927723449299, 3.035229711104609596, -3.433252694550591233 ) ) ;
#3127=ORIENTED_EDGE ( 'NONE', *, *, #5203, .F. ) ;
#3129=CARTESIAN_POINT ( 'NONE',  ( 5.560781378645575757, 0.000000000000000000, -4.000000000000000000 ) ) ;
#3140=CARTESIAN_POINT ( 'NONE',  ( 4.000000000000000000, -1.084202172485504434E-14, -3.142992957459231906 ) ) ;
#3154=LINE ( 'NONE', #5445, #6745 ) ;
#3167=ADVANCED_FACE ( 'NONE', ( #10381 ), #6891, .F. ) ;
#3200=CARTESIAN_POINT ( 'NONE',  ( -1.240299975428134203E-15, -4.736529461165891242, -3.681130640444276292 ) ) ;
#3207=DIRECTION ( 'NONE',  ( 0.000000000000000000, 0.000000000000000000, 1.000000000000000000 ) ) ;
#3221=LINE ( 'NONE', #989, #5070 ) ;
#3228=EDGE_CURVE ( 'NONE', #10246, #5348, #11338, .T. ) ;
#3249=ADVANCED_FACE ( 'NONE', ( #9147 ), #12203, .T. ) ;
#3256=DIRECTION ( 'NONE',  ( -0.000000000000000000, -0.000000000000000000, 1.000000000000000000 ) ) ;
#3261=B_SPLINE_CURVE_WITH_KNOTS ( 'NONE', 3,
 ( #4796, #8116, #9082, #3826, #11072, #4868, #1527, #12256 ),
 .UNSPECIFIED., .F., .F.,
 ( 4, 2, 2, 4 ),
 ( 2.465131517390770070E-07, 0.001183067374689869946, 0.001774477805458935659, 0.002365888236228001588 ),
 .UNSPECIFIED. ) ;
#3263=VERTEX_POINT ( 'NONE', #5071 ) ;
#3289=CARTESIAN_POINT ( 'NONE',  ( 0.6937372685066666156, -4.453844082567737672, -3.610536846335894445 ) ) ;
#3302=FACE_OUTER_BOUND ( 'NONE', #12491, .T. ) ;
#3320=EDGE_CURVE ( 'NONE', #4810, #3920, #695, .T. ) ;
#3333=CARTESIAN_POINT ( 'NONE',  ( -2.682243648011671588, -3.070208061305317759, -0.04852650426602272971 ) ) ;
#3347=ORIENTED_EDGE ( 'NONE', *, *, #11556, .T. ) ;
#3354=CARTESIAN_POINT ( 'NONE',  ( -4.000000000000000000, -2.309401076758515803, -0.4999999999999995559 ) ) ;
#3358=FACE_OUTER_BOUND ( 'NONE', #7641, .T. ) ;
#3371=CARTESIAN_POINT ( 'NONE',  ( -2.171643655288372443, 3.365003104552320767, 2.541098841762897165E-18 ) ) ;
#3390=PLANE ( 'NONE',  #10370 ) ;
#3405=CARTESIAN_POINT ( 'NONE',  ( 1.317756351988342622, -3.857995168970215438, -0.04852650426602527628 ) ) ;
#3415=CONICAL_SURFACE ( 'NONE', #3425, 4.000000000000000000, 0.8911886515913786111 ) ;
#3423=SURFACE_STYLE_FILL_AREA ( #8683 ) ;
#3425=AXIS2_PLACEMENT_3D ( 'NONE', #7258, #6096, #7330 ) ;
#3426=CARTESIAN_POINT ( 'NONE',  ( 3.511755186886750923, -2.826662030176382956, -3.597382984111582083 ) ) ;
#3434=VERTEX_POINT ( 'NONE', #9821 ) ;
#3438=CARTESIAN_POINT ( 'NONE',  ( 0.6920835326022565237, 4.454600218803884459, -3.597382984111579862 ) ) ;
#3471=DIRECTION ( 'NONE',  ( 1.000000000000000000, 0.000000000000000000, 0.000000000000000000 ) ) ;
#3478=DIRECTION ( 'NONE',  ( -0.5000000000000016653, 0.8660254037844378194, 0.000000000000000000 ) ) ;
#3484=CARTESIAN_POINT ( 'NONE',  ( -3.510273485745307287, -2.827716139362669967, -3.610536846335890004 ) ) ;
#3487=EDGE_CURVE ( 'NONE', #6427, #4186, #763, .T. ) ;
#3493=CARTESIAN_POINT ( 'NONE',  ( 0.000000000000000000, 0.000000000000000000, -4.000000000000000000 ) ) ;
#3494=CARTESIAN_POINT ( 'NONE',  ( 4.000000000000000000, 0.000000000000000000, 0.000000000000000000 ) ) ;
#3496=CARTESIAN_POINT ( 'NONE',  ( 4.154306624731035846, -2.398490048085128556, -3.721999068284417955 ) ) ;
#3545=CARTESIAN_POINT ( 'NONE',  ( 0.000000000000000000, 0.000000000000000000, -4.000000000000000000 ) ) ;
#3550=CARTESIAN_POINT ( 'NONE',  ( -3.974344831685191280E-13, 4.796734841935104576, -3.721909803043223608 ) ) ;
#3573=EDGE_LOOP ( 'NONE', ( #10694, #10646, #10741, #7536, #4165 ) ) ;
#3575=CARTESIAN_POINT ( 'NONE',  ( -0.1750025118121544265, -4.719839900820635314, -3.469254087858253399 ) ) ;
#3576=CARTESIAN_POINT ( 'NONE',  ( -2.059999999999998721, 2.522772406243545965E-16, -0.3080913168122742518 ) ) ;
#3617=DIRECTION ( 'NONE',  ( -0.000000000000000000, -0.000000000000000000, 1.000000000000000000 ) ) ;
#3636=DIRECTION ( 'NONE',  ( -0.000000000000000000, 0.000000000000000000, -1.000000000000000000 ) ) ;
#3653=ORIENTED_EDGE ( 'NONE', *, *, #3874, .T. ) ;
#3661=EDGE_CURVE ( 'NONE', #11968, #9204, #7802, .T. ) ;
#3663=CARTESIAN_POINT ( 'NONE',  ( -4.000000000000000000, 2.309401076758498483, -3.433295621305379353 ) ) ;
#3665=EDGE_CURVE ( 'NONE', #5544, #4712, #12310, .T. ) ;
#3676=CARTESIAN_POINT ( 'NONE',  ( 0.000000000000000000, 0.000000000000000000, -0.3080913168122742518 ) ) ;
#3722=CARTESIAN_POINT ( 'NONE',  ( 4.000000000000000000, -2.471525695159793035, -3.686886880705770864 ) ) ;
#3726=ADVANCED_FACE ( 'NONE', ( #4989 ), #5386, .F. ) ;
#3752=ORIENTED_EDGE ( 'NONE', *, *, #8841, .F. ) ;
#3753=CONICAL_SURFACE ( 'NONE', #8176, 4.000000000000000000, 0.8911886515913786111 ) ;
#3764=DIRECTION ( 'NONE',  ( -1.000000000000000000, 0.000000000000000000, 0.000000000000000000 ) ) ;
#3771=VERTEX_POINT ( 'NONE', #7267 ) ;
#3784=CIRCLE ( 'NONE', #10841, 0.5155456020628804703 ) ;
#3793=CIRCLE ( 'NONE', #13491, 5.560781378645573980 ) ;
#3826=CARTESIAN_POINT ( 'NONE',  ( -1.144235203016679359, -3.958177651039096911, -0.09382832055446428676 ) ) ;
#3858=ORIENTED_EDGE ( 'NONE', *, *, #1435, .T. ) ;
#3861=FACE_OUTER_BOUND ( 'NONE', #566, .T. ) ;
#3865=CARTESIAN_POINT ( 'NONE',  ( 4.000000000000000000, 1.680228229147133767, -3.316631783032546021 ) ) ;
#3874=EDGE_CURVE ( 'NONE', #4365, #6658, #7719, .T. ) ;
#3905=EDGE_LOOP ( 'NONE', ( #4499, #1424, #7220, #10201 ) ) ;
#3920=VERTEX_POINT ( 'NONE', #1470 ) ;
#3947=CARTESIAN_POINT ( 'NONE',  ( 4.211140560182196957, 2.431303136016536470, -3.745885042887433514 ) ) ;
#3955=EDGE_LOOP ( 'NONE', ( #3752, #9829, #13189, #13078, #2469 ) ) ;
#3978=LINE ( 'NONE', #847, #1502 ) ;
#3989=FACE_OUTER_BOUND ( 'NONE', #4848, .T. ) ;
#3996=B_SPLINE_CURVE_WITH_KNOTS ( 'NONE', 3,
 ( #5508, #3426, #301, #11854, #6608, #3289, #4388, #7714 ),
 .UNSPECIFIED., .F., .F.,
 ( 4, 2, 2, 4 ),
 ( 0.000000000000000000, 0.002450665683189819262, 0.003675998524784728893, 0.004901331366379639391 ),
 .UNSPECIFIED. ) ;
#4024=EDGE_CURVE ( 'NONE', #1117, #4810, #10475, .T. ) ;
#4027=CARTESIAN_POINT ( 'NONE',  ( -4.204114297095464359, 1.660363174096617156, -3.602136431857887011 ) ) ;
#4067=( BOUNDED_SURFACE ( )  B_SPLINE_SURFACE ( 3, 2, ( 
 ( #11562, #2072, #7278 ),
 ( #11489, #5141, #13544 ),
 ( #13470, #3117, #4291 ),
 ( #9279, #420, #1869 ),
 ( #9349, #12650, #8379 ),
 ( #2008, #5066, #1934 ) ),
 .UNSPECIFIED., .F., .F., .F. ) 
 B_SPLINE_SURFACE_WITH_KNOTS ( ( 4, 2, 4 ),
 ( 3, 3 ),
 ( 0.02032853247518126225, 0.02278863295364821212, 0.02524873343211516200 ),
 ( 0.000000000000000000, 1.000000000000000000 ),
 .UNSPECIFIED. ) 
 GEOMETRIC_REPRESENTATION_ITEM ( )  RATIONAL_B_SPLINE_SURFACE ( (
 ( 1.000000000000000000, 0.8047781615896835161, 1.000000000000000000),
 ( 1.000000000000000000, 0.8123767586291043008, 1.000000000000000000),
 ( 1.000000000000000000, 0.8190662415562011134, 1.000000000000000000),
 ( 1.000000000000000000, 0.8192361015671398849, 1.000000000000000000),
 ( 1.000000000000000000, 0.8126135807102121689, 1.000000000000000000),
 ( 1.000000000000000000, 0.8047712338318585568, 1.000000000000000000) ) ) 
 REPRESENTATION_ITEM ( '' )  SURFACE ( )  );
#4099=CARTESIAN_POINT ( 'NONE',  ( 3.999999999999999112, 1.941961291383486277, -0.3515519931180248192 ) ) ;
#4113=CARTESIAN_POINT ( 'NONE',  ( 0.000000000000000000, 0.000000000000000000, 3.469446951953614189E-15 ) ) ;
#4118=CARTESIAN_POINT ( 'NONE',  ( 4.000000000000000000, -2.309401076758514915, -3.433295621305383349 ) ) ;
#4133=CARTESIAN_POINT ( 'NONE',  ( 3.999999999999999112, -0.3979232138631231819, -5.929230630780099908E-17 ) ) ;
#4161=EDGE_CURVE ( 'NONE', #10246, #7551, #7607, .T. ) ;
#4165=ORIENTED_EDGE ( 'NONE', *, *, #6018, .F. ) ;
#4186=VERTEX_POINT ( 'NONE', #3075 ) ;
#4189=VERTEX_POINT ( 'NONE', #7310 ) ;
#4196=CARTESIAN_POINT ( 'NONE',  ( -0.5276280594146446346, 4.314175951381965746, -3.320322319201721495 ) ) ;
#4215=AXIS2_PLACEMENT_3D ( 'NONE', #5674, #2476, #2545 ) ;
#4223=CARTESIAN_POINT ( 'NONE',  ( 0.000000000000000000, 0.000000000000000000, -4.974599999999998801 ) ) ;
#4238=CARTESIAN_POINT ( 'NONE',  ( -4.000000000000000888, -2.309401076758512694, -3.504269196027526512 ) ) ;
#4266=CARTESIAN_POINT ( 'NONE',  ( -2.712762565639006418, 3.052587955997511759, -3.430618716626627318 ) ) ;
#4268=CARTESIAN_POINT ( 'NONE',  ( -4.000000000000000000, 0.000000000000000000, 0.000000000000000000 ) ) ;
#4291=CARTESIAN_POINT ( 'NONE',  ( 2.836893136758676270, 3.208949435745843903, -3.505054077164911241 ) ) ;
#4301=EDGE_LOOP ( 'NONE', ( #10520, #13620, #3858, #1629 ) ) ;
#4335=ORIENTED_EDGE ( 'NONE', *, *, #11163, .F. ) ;
#4337=CIRCLE ( 'NONE', #8322, 0.5155456020628804703 ) ;
#4340=ORIENTED_EDGE ( 'NONE', *, *, #8568, .F. ) ;
#4343=DIRECTION ( 'NONE',  ( 0.000000000000000000, 0.000000000000000000, -1.000000000000000000 ) ) ;
#4365=VERTEX_POINT ( 'NONE', #4118 ) ;
#4371=CARTESIAN_POINT ( 'NONE',  ( 0.3208286057739604957, -4.433571671609698228, -0.3503314178412692548 ) ) ;
#4377=DIRECTION ( 'NONE',  ( 0.8660254037844379305, 0.5000000000000013323, 0.000000000000000000 ) ) ;
#4388=CARTESIAN_POINT ( 'NONE',  ( 0.3461262719736147297, -4.658553426539303821, -3.671615880910379381 ) ) ;
#4396=CIRCLE ( 'NONE', #6185, 4.000000000000000000 ) ;
#4405=CARTESIAN_POINT ( 'NONE',  ( 3.510273485745307731, 2.827716139362654424, -3.610536846335885564 ) ) ;
#4417=COLOUR_RGB ( '',1.000000000000000000, 0.9490196078431372140, 0.9098039215686274384 ) ;
#4426=DIRECTION ( 'NONE',  ( 0.000000000000000000, 0.000000000000000000, -1.000000000000000000 ) ) ;
#4434=ORIENTED_EDGE ( 'NONE', *, *, #12541, .T. ) ;
#4435=CARTESIAN_POINT ( 'NONE',  ( -3.349226789952655547, -2.685125164760744809, -0.2236248678334863682 ) ) ;
#4439=EDGE_CURVE ( 'NONE', #4365, #4606, #6007, .T. ) ;
#4465=AXIS2_PLACEMENT_3D ( 'NONE', #12308, #13542, #1023 ) ;
#4485=ORIENTED_EDGE ( 'NONE', *, *, #11334, .F. ) ;
#4499=ORIENTED_EDGE ( 'NONE', *, *, #7118, .F. ) ;
#4509=CARTESIAN_POINT ( 'NONE',  ( 0.6507732100473444525, -4.243078065514795050, -0.2236248678334952777 ) ) ;
#4516=DIRECTION ( 'NONE',  ( 0.000000000000000000, 0.000000000000000000, 1.000000000000000000 ) ) ;
#4527=( NAMED_UNIT ( * ) SI_UNIT ( $, .STERADIAN. ) SOLID_ANGLE_UNIT ( ) );
#4543=FACE_OUTER_BOUND ( 'NONE', #8308, .T. ) ;
#4547=CARTESIAN_POINT ( 'NONE',  ( 4.154306624731137099, 2.398490048084935822, -3.721999068284414847 ) ) ;
#4558=EDGE_LOOP ( 'NONE', ( #12424, #7520, #10524, #12788 ) ) ;
#4586=CARTESIAN_POINT ( 'NONE',  ( 1.567478505476134606E-15, 4.618802153517012066, -5.000000000000000000 ) ) ;
#4592=DIRECTION ( 'NONE',  ( -1.000000000000000000, 0.000000000000000000, 0.000000000000000000 ) ) ;
#4606=VERTEX_POINT ( 'NONE', #12148 ) ;
#4609=ORIENTED_EDGE ( 'NONE', *, *, #9240, .T. ) ;
#4612=CARTESIAN_POINT ( 'NONE',  ( 4.236525694536557474, -2.416953475386482530, -3.751298745799839462 ) ) ;
#4658=CARTESIAN_POINT ( 'NONE',  ( -0.6937372685066653943, 4.453844082567723461, -3.610536846335889116 ) ) ;
#4680=CARTESIAN_POINT ( 'NONE',  ( 4.207491450040567571, -2.029819825146485179, -3.671670828759567407 ) ) ;
#4712=VERTEX_POINT ( 'NONE', #8422 ) ;
#4713=ORIENTED_EDGE ( 'NONE', *, *, #11474, .T. ) ;
#4723=ADVANCED_FACE ( 'NONE', ( #7180 ), #322, .T. ) ;
#4745=ADVANCED_FACE ( 'NONE', ( #3989 ), #5109, .T. ) ;
#4749=CARTESIAN_POINT ( 'NONE',  ( 2.345747346278113987, -3.264484291692503870, -0.01223254789874484924 ) ) ;
#4753=CARTESIAN_POINT ( 'NONE',  ( -2.500000000000000444, 3.061616997868383634E-16, -25.03750572909317285 ) ) ;
#4764=ORIENTED_EDGE ( 'NONE', *, *, #11163, .T. ) ;
#4771=CARTESIAN_POINT ( 'NONE',  ( -4.197393957002303999, 0.4069871074557429025, -3.503767560748926257 ) ) ;
#4776=ORIENTED_EDGE ( 'NONE', *, *, #928, .F. ) ;
#4779=CIRCLE ( 'NONE', #7434, 5.384454397937118664 ) ;
#4796=CARTESIAN_POINT ( 'NONE',  ( -2.688821387764050996E-14, -4.618802153517012954, -0.4999999999999995559 ) ) ;
#4803=B_SPLINE_CURVE_WITH_KNOTS ( 'NONE', 3,
 ( #13424, #9089, #7159, #7087, #1889 ),
 .UNSPECIFIED., .F., .F.,
 ( 4, 1, 4 ),
 ( 0.000000000000000000, 0.002309401076758505790, 0.004618802153517011580 ),
 .UNSPECIFIED. ) ;
#4810=VERTEX_POINT ( 'NONE', #4268 ) ;
#4828=ORIENTED_EDGE ( 'NONE', *, *, #9240, .F. ) ;
#4848=EDGE_LOOP ( 'NONE', ( #2114, #8221, #11912, #10757, #309 ) ) ;
#4854=DIRECTION ( 'NONE',  ( -0.000000000000000000, -0.000000000000000000, 1.000000000000000000 ) ) ;
#4855=PRODUCT_DEFINITION_FORMATION_WITH_SPECIFIED_SOURCE ( 'ANY', '', #13478, .NOT_KNOWN. ) ;
#4868=CARTESIAN_POINT ( 'NONE',  ( -1.654252653721913102, -3.663718938583024443, -0.01223254789874440342 ) ) ;
#4881=DIRECTION ( 'NONE',  ( 0.000000000000000000, 0.000000000000000000, 1.000000000000000000 ) ) ;
#4884=CARTESIAN_POINT ( 'NONE',  ( 0.000000000000000000, 0.000000000000000000, 0.000000000000000000 ) ) ;
#4898=CIRCLE ( 'NONE', #11526, 2.100000000000000089 ) ;
#4912=CARTESIAN_POINT ( 'NONE',  ( 4.000000000000000888, -0.8578082829538523635, -3.433262215449808696 ) ) ;
#4916=CARTESIAN_POINT ( 'NONE',  ( -4.197393957002303999, -0.8151795401431414234, -3.503767560748935139 ) ) ;
#4922=ORIENTED_EDGE ( 'NONE', *, *, #3228, .T. ) ;
#4924=CARTESIAN_POINT ( 'NONE',  ( -2.449848172108560540, -3.432307619358754724, -3.503702292528910078 ) ) ;
#4927=CARTESIAN_POINT ( 'NONE',  ( 0.000000000000000000, 0.000000000000000000, 3.469446951953614189E-15 ) ) ;
#4934=CARTESIAN_POINT ( 'NONE',  ( 4.000000000000000000, 2.309401076758515803, -0.4999999999999995559 ) ) ;
#4935=EDGE_CURVE ( 'NONE', #4186, #12042, #4803, .T. ) ;
#4939=ORIENTED_EDGE ( 'NONE', *, *, #5049, .F. ) ;
#4941=CARTESIAN_POINT ( 'NONE',  ( 0.6448876103708359731, 4.246476118072354922, -0.2256878752776725616 ) ) ;
#4989=FACE_OUTER_BOUND ( 'NONE', #4558, .T. ) ;
#4994=FACE_OUTER_BOUND ( 'NONE', #11553, .T. ) ;
#5049=EDGE_CURVE ( 'NONE', #4365, #5652, #2640, .T. ) ;
#5054=CARTESIAN_POINT ( 'NONE',  ( 4.197310751797292738, 0.8178363989516252985, -3.502498386812444409 ) ) ;
#5066=CARTESIAN_POINT ( 'NONE',  ( -0.1410422978106123659, 4.700232962125094893, -3.687027686973624707 ) ) ;
#5070=VECTOR ( 'NONE', #7443, 1000.000000000000000 ) ;
#5071=CARTESIAN_POINT ( 'NONE',  ( 2.500000000000000444, 0.000000000000000000, -5.000000000000000888 ) ) ;
#5083=VECTOR ( 'NONE', #730, 1000.000000000000000 ) ;
#5092=DIRECTION ( 'NONE',  ( -1.000000000000000000, 0.000000000000000000, 0.000000000000000000 ) ) ;
#5109=PLANE ( 'NONE',  #11137 ) ;
#5110=CARTESIAN_POINT ( 'NONE',  ( 4.000000000000000000, -1.560351142792952617, -0.2242961665059816367 ) ) ;
#5116=AXIS2_PLACEMENT_3D ( 'NONE', #5139, #2986, #8443 ) ;
#5126=CARTESIAN_POINT ( 'NONE',  ( -4.000000000000000000, 1.941961291383472732, -0.3515519931180205448 ) ) ;
#5135=B_SPLINE_CURVE_WITH_KNOTS ( 'NONE', 3,
 ( #7583, #7854, #8619, #1259, #12065, #9853 ),
 .UNSPECIFIED., .F., .F.,
 ( 4, 2, 4 ),
 ( 0.002365888236227995517, 0.003551327329835084114, 0.004736766423442172712 ),
 .UNSPECIFIED. ) ;
#5139=CARTESIAN_POINT ( 'NONE',  ( 0.000000000000000000, 0.000000000000000000, 0.000000000000000000 ) ) ;
#5141=CARTESIAN_POINT ( 'NONE',  ( 3.453038570460273071, 2.625189405340834448, -3.535263753543585352 ) ) ;
#5147=CARTESIAN_POINT ( 'NONE',  ( 4.000000000000000000, 0.7924765000094659007, -0.05906175389889852662 ) ) ;
#5155=LINE ( 'NONE', #9690, #1441 ) ;
#5178=CARTESIAN_POINT ( 'NONE',  ( -2.807080416178626692, 3.225969019225154444, -3.502507215260441065 ) ) ;
#5197=EDGE_CURVE ( 'NONE', #6904, #6584, #10399, .T. ) ;
#5203=EDGE_CURVE ( 'NONE', #9576, #5420, #7345, .T. ) ;
#5211=EDGE_CURVE ( 'NONE', #2490, #10214, #1122, .T. ) ;
#5222=EDGE_LOOP ( 'NONE', ( #12478, #8571, #8386, #7811 ) ) ;
#5255=CARTESIAN_POINT ( 'NONE',  ( -0.6810597143197697489, -4.461075778259609770, -3.598441714920717516 ) ) ;
#5301=ORIENTED_EDGE ( 'NONE', *, *, #12335, .T. ) ;
#5311=CARTESIAN_POINT ( 'NONE',  ( -1.243802165048909503, 3.900692638707381921, -3.223146290109805800 ) ) ;
#5319=CARTESIAN_POINT ( 'NONE',  ( -1.390230914382372118, -4.043987460488664532, -3.502507215260523665 ) ) ;
#5337=VECTOR ( 'NONE', #12075, 999.9999999999998863 ) ;
#5348=VERTEX_POINT ( 'NONE', #13001 ) ;
#5350=EDGE_LOOP ( 'NONE', ( #2275, #8805, #7287, #4434, #7792 ) ) ;
#5355=CARTESIAN_POINT ( 'NONE',  ( -4.211140560182196957, -2.431303136016552013, -3.745885042887436178 ) ) ;
#5371=FACE_OUTER_BOUND ( 'NONE', #3573, .T. ) ;
#5374=AXIS2_PLACEMENT_3D ( 'NONE', #7436, #10734, #4377 ) ;
#5386=CYLINDRICAL_SURFACE ( 'NONE', #1596, 2.100000000000000089 ) ;
#5420=VERTEX_POINT ( 'NONE', #13533 ) ;
#5434=CARTESIAN_POINT ( 'NONE',  ( 0.000000000000000000, 0.000000000000000000, -5.000000000000000888 ) ) ;
#5440=CARTESIAN_POINT ( 'NONE',  ( 1.411581201560190495E-15, 4.862606272033091592, -3.745885042887436622 ) ) ;
#5445=CARTESIAN_POINT ( 'NONE',  ( -2.500000000000000888, 0.000000000000000000, -4.974599999999998801 ) ) ;
#5446=CARTESIAN_POINT ( 'NONE',  ( 2.000000000000008882, 3.464101615137749945, 0.000000000000000000 ) ) ;
#5450=DIRECTION ( 'NONE',  ( -0.000000000000000000, -0.000000000000000000, 1.000000000000000000 ) ) ;
#5477=DIRECTION ( 'NONE',  ( -0.000000000000000000, 0.000000000000000000, -1.000000000000000000 ) ) ;
#5499=CARTESIAN_POINT ( 'NONE',  ( 1.567478505476134606E-15, 4.618802153517012066, -3.433295621305382905 ) ) ;
#5506=( LENGTH_UNIT ( ) NAMED_UNIT ( * ) SI_UNIT ( .MILLI., .METRE. ) );
#5508=CARTESIAN_POINT ( 'NONE',  ( 4.211140560182196957, -2.431303136016555122, -3.745885042887436622 ) ) ;
#5517=CARTESIAN_POINT ( 'NONE',  ( 0.1756481739660539498, -4.720212674038995360, -3.469390959564070620 ) ) ;
#5526=EDGE_CURVE ( 'NONE', #13574, #10214, #11476, .T. ) ;
#5535=CARTESIAN_POINT ( 'NONE',  ( 2.100000000000000089, 0.000000000000000000, -0.2800830152838844622 ) ) ;
#5538=CIRCLE ( 'NONE', #12596, 2.499999999999999556 ) ;
#5544=VERTEX_POINT ( 'NONE', #12903 ) ;
#5563=ORIENTED_EDGE ( 'NONE', *, *, #11474, .F. ) ;
#5651=CARTESIAN_POINT ( 'NONE',  ( 4.101954839143059139, -2.368264730582948285, -3.681130640444269631 ) ) ;
#5652=VERTEX_POINT ( 'NONE', #9868 ) ;
#5653=EDGE_LOOP ( 'NONE', ( #8541, #8558, #11660, #6376 ) ) ;
#5656=CARTESIAN_POINT ( 'NONE',  ( 2.725741868436127202, -3.045094352033990148, -3.220599429844051453 ) ) ;
#5657=DIRECTION ( 'NONE',  ( -0.9396926207859138680, 0.000000000000000000, -0.3420201433256536139 ) ) ;
#5674=CARTESIAN_POINT ( 'NONE',  ( 0.000000000000000000, 0.000000000000000000, -4.000000000000000000 ) ) ;
#5675=AXIS2_PLACEMENT_3D ( 'NONE', #4223, #3256, #12445 ) ;
#5712=CARTESIAN_POINT ( 'NONE',  ( -2.500000000000000444, 3.061616997868383634E-16, -5.000000000000000888 ) ) ;
#5714=MANIFOLD_SOLID_BREP ( 'EndChamfer', #7149 ) ;
#5745=VECTOR ( 'NONE', #3207, 1000.000000000000000 ) ;
#5749=CARTESIAN_POINT ( 'NONE',  ( -4.211140560182196957, 2.431303136016537803, -3.745885042887433514 ) ) ;
#5759=TOROIDAL_SURFACE ( 'NONE', #13459, 5.384454397937118664, 0.5155456020628804703 ) ;
#5798=AXIS2_PLACEMENT_3D ( 'NONE', #914, #6341, #5092 ) ;
#5823=VERTEX_POINT ( 'NONE', #10204 ) ;
#5828=CARTESIAN_POINT ( 'NONE',  ( 0.000000000000000000, 0.000000000000000000, 0.000000000000000000 ) ) ;
#5830=CARTESIAN_POINT ( 'NONE',  ( -6.259644161404860030E-16, -4.618802153517027165, -3.433295621305388234 ) ) ;
#5858=ORIENTED_EDGE ( 'NONE', *, *, #5211, .F. ) ;
#5877=ORIENTED_EDGE ( 'NONE', *, *, #12263, .F. ) ;
#5882=CARTESIAN_POINT ( 'NONE',  ( 4.197478902586992966, -0.8524102783748346290, -3.505063281295504041 ) ) ;
#5938=APPLICATION_CONTEXT ( 'automotive_design' ) ;
#5940=EDGE_CURVE ( 'NONE', #11968, #5420, #860, .T. ) ;
#5943=ORIENTED_EDGE ( 'NONE', *, *, #7215, .T. ) ;
#5954=FACE_OUTER_BOUND ( 'NONE', #969, .T. ) ;
#5963=ORIENTED_EDGE ( 'NONE', *, *, #3487, .T. ) ;
#5983=ORIENTED_EDGE ( 'NONE', *, *, #5940, .F. ) ;
#5999=CARTESIAN_POINT ( 'NONE',  ( 4.000000000000000000, 2.309401076758497151, -3.433295621305379353 ) ) ;
#6007=LINE ( 'NONE', #9111, #11599 ) ;
#6018=EDGE_CURVE ( 'NONE', #4606, #10246, #12052, .T. ) ;
#6019=CARTESIAN_POINT ( 'NONE',  ( -2.000000000000002665, -3.464101615137770374, -3.142992957459237680 ) ) ;
#6040=CARTESIAN_POINT ( 'NONE',  ( -4.211140560182196957, -2.431303136016552013, -3.745885042887436178 ) ) ;
#6049=CARTESIAN_POINT ( 'NONE',  ( 4.000000000000000000, 0.000000000000000000, 0.000000000000000000 ) ) ;
#6055=ORIENTED_EDGE ( 'NONE', *, *, #883, .F. ) ;
#6056=EDGE_CURVE ( 'NONE', #7551, #5348, #5135, .T. ) ;
#6061=PRODUCT_CONTEXT ( 'NONE', #10163, 'mechanical' ) ;
#6078=FACE_OUTER_BOUND ( 'NONE', #4301, .T. ) ;
#6096=DIRECTION ( 'NONE',  ( 0.000000000000000000, 0.000000000000000000, -1.000000000000000000 ) ) ;
#6141=ORIENTED_EDGE ( 'NONE', *, *, #8531, .F. ) ;
#6150=CARTESIAN_POINT ( 'NONE',  ( -1.257172072275743346, 3.892973519171203378, -3.433252694550776862 ) ) ;
#6161=DIRECTION ( 'NONE',  ( -0.000000000000000000, -0.000000000000000000, 1.000000000000000000 ) ) ;
#6165=CARTESIAN_POINT ( 'NONE',  ( -4.000000000000000888, 1.563622288139195238, -0.2253451193528307472 ) ) ;
#6185=AXIS2_PLACEMENT_3D ( 'NONE', #8808, #11988, #4592 ) ;
#6191=ORIENTED_EDGE ( 'NONE', *, *, #2727, .T. ) ;
#6212=CARTESIAN_POINT ( 'NONE',  ( 4.000000000000000000, 2.309401076758497151, -5.000000000000000000 ) ) ;
#6232=B_SPLINE_CURVE_WITH_KNOTS ( 'NONE', 3,
 ( #7926, #7798, #7863, #2525, #4680, #8963 ),
 .UNSPECIFIED., .F., .F.,
 ( 4, 2, 4 ),
 ( 0.002452478801916361129, 0.003676905084148001344, 0.004901331366379641126 ),
 .UNSPECIFIED. ) ;
#6240=AXIS2_PLACEMENT_3D ( 'NONE', #7781, #2371, #12123 ) ;
#6249=ORIENTED_EDGE ( 'NONE', *, *, #1435, .F. ) ;
#6261=CARTESIAN_POINT ( 'NONE',  ( -4.211405944401398038, -2.460460786169389902, -3.751298493805494072 ) ) ;
#6263=ORIENTED_EDGE ( 'NONE', *, *, #2727, .F. ) ;
#6282=ADVANCED_FACE ( 'NONE', ( #13217 ), #1537, .T. ) ;
#6302=DIRECTION ( 'NONE',  ( -0.000000000000000000, -0.000000000000000000, 1.000000000000000000 ) ) ;
#6307=CARTESIAN_POINT ( 'NONE',  ( -4.000000000000000000, 0.1981133338132459731, 2.096406544454392723E-17 ) ) ;
#6326=CARTESIAN_POINT ( 'NONE',  ( -4.000000000000000000, -2.472261339043343220, -3.687027428081192326 ) ) ;
#6329=ORIENTED_EDGE ( 'NONE', *, *, #9559, .F. ) ;
#6341=DIRECTION ( 'NONE',  ( 0.000000000000000000, 0.000000000000000000, -1.000000000000000000 ) ) ;
#6371=ADVANCED_FACE ( 'NONE', ( #10330 ), #8448, .F. ) ;
#6376=ORIENTED_EDGE ( 'NONE', *, *, #12335, .F. ) ;
#6401=VECTOR ( 'NONE', #11590, 1000.000000000000000 ) ;
#6402=CARTESIAN_POINT ( 'NONE',  ( -2.100000000000000089, 2.571758278209441957E-16, -5.000000000000000000 ) ) ;
#6404=AXIS2_PLACEMENT_3D ( 'NONE', #627, #3764, #4881 ) ;
#6427=VERTEX_POINT ( 'NONE', #13570 ) ;
#6429=CARTESIAN_POINT ( 'NONE',  ( -2.836893136758495970, -3.208949435745868328, -3.505054077164885484 ) ) ;
#6431=CARTESIAN_POINT ( 'NONE',  ( -6.259644161404860030E-16, -4.618802153517027165, -5.000000000000000000 ) ) ;
#6463=CARTESIAN_POINT ( 'NONE',  ( -4.024497503033519941, -2.323544716729390558, -3.572167766733381544 ) ) ;
#6477=CARTESIAN_POINT ( 'NONE',  ( 2.290893957444128645E-15, 4.647089433458768681, -3.572167766733382877 ) ) ;
#6488=CARTESIAN_POINT ( 'NONE',  ( 4.000000000000000000, -1.942223658245635809, -0.3516579909967643691 ) ) ;
#6522=ORIENTED_EDGE ( 'NONE', *, *, #2576, .F. ) ;
#6529=DIRECTION ( 'NONE',  ( -0.000000000000000000, -0.000000000000000000, 1.000000000000000000 ) ) ;
#6546=( NAMED_UNIT ( * ) PLANE_ANGLE_UNIT ( ) SI_UNIT ( $, .RADIAN. ) );
#6584=VERTEX_POINT ( 'NONE', #6996 ) ;
#6608=CARTESIAN_POINT ( 'NONE',  ( 1.393927851585479161, -4.043713361053543842, -3.526374918436840922 ) ) ;
#6618=EDGE_CURVE ( 'NONE', #9204, #11968, #11302, .T. ) ;
#6626=( GEOMETRIC_REPRESENTATION_CONTEXT ( 3 ) GLOBAL_UNCERTAINTY_ASSIGNED_CONTEXT ( ( #12823 ) ) GLOBAL_UNIT_ASSIGNED_CONTEXT ( ( #7576, #6546, #4527 ) ) REPRESENTATION_CONTEXT ( 'NONE', 'WORKASPACE' ) );
#6640=ADVANCED_FACE ( 'NONE', ( #2775 ), #13467, .F. ) ;
#6658=VERTEX_POINT ( 'NONE', #3115 ) ;
#6659=CARTESIAN_POINT ( 'NONE',  ( -4.000000000000000000, -2.309401076758515803, -0.4999999999999995559 ) ) ;
#6667=DIRECTION ( 'NONE',  ( -1.000000000000000000, 0.000000000000000000, 0.000000000000000000 ) ) ;
#6682=CARTESIAN_POINT ( 'NONE',  ( 0.000000000000000000, 0.000000000000000000, -0.3080913168122742518 ) ) ;
#6728=CARTESIAN_POINT ( 'NONE',  ( -2.000000000000007550, -3.464101615137749945, 0.000000000000000000 ) ) ;
#6745=VECTOR ( 'NONE', #11591, 1000.000000000000114 ) ;
#6752=ORIENTED_EDGE ( 'NONE', *, *, #2758, .T. ) ;
#6802=ORIENTED_EDGE ( 'NONE', *, *, #687, .F. ) ;
#6823=CARTESIAN_POINT ( 'NONE',  ( 0.000000000000000000, 0.000000000000000000, -4.974599999999998801 ) ) ;
#6840=CARTESIAN_POINT ( 'NONE',  ( 4.000000000000000000, -1.677850389431204459, -3.535268758346977513 ) ) ;
#6890=CARTESIAN_POINT ( 'NONE',  ( 4.141042297810615835, -2.227970268150433863, -3.687027686973623819 ) ) ;
#6891=( BOUNDED_SURFACE ( )  B_SPLINE_SURFACE ( 3, 2, ( 
 ( #7355, #11566, #13617 ),
 ( #10241, #12314, #4027 ),
 ( #7145, #755, #12521 ),
 ( #13405, #11494, #818 ),
 ( #2991, #7214, #12451 ),
 ( #2077, #6326, #6261 ) ),
 .UNSPECIFIED., .F., .F., .F. ) 
 B_SPLINE_SURFACE_WITH_KNOTS ( ( 4, 2, 4 ),
 ( 3, 3 ),
 ( 0.02027752710269158445, 0.02273781595091097299, 0.02519810479913036153 ),
 ( 0.000000000000000000, 1.000000000000000000 ),
 .UNSPECIFIED. ) 
 GEOMETRIC_REPRESENTATION_ITEM ( )  RATIONAL_B_SPLINE_SURFACE ( (
 ( 1.000000000000000000, 0.8047781431712808242, 1.000000000000000000),
 ( 1.000000000000000000, 0.8123773247083928561, 1.000000000000000000),
 ( 1.000000000000000000, 0.8190670192154906326, 1.000000000000000000),
 ( 1.000000000000000000, 0.8192353552912178261, 1.000000000000000000),
 ( 1.000000000000000000, 0.8126132098226825917, 1.000000000000000000),
 ( 1.000000000000000000, 0.8047712465856394770, 1.000000000000000000) ) ) 
 REPRESENTATION_ITEM ( '' )  SURFACE ( )  );
#6904=VERTEX_POINT ( 'NONE', #8905 ) ;
#6933=B_SPLINE_CURVE_WITH_KNOTS ( 'NONE', 3,
 ( #3354, #12683, #8350, #169, #11651, #1194 ),
 .UNSPECIFIED., .F., .F.,
 ( 4, 2, 4 ),
 ( 0.003358874760055550156, 0.004541967308452096383, 0.005725059856848641743 ),
 .UNSPECIFIED. ) ;
#6962=CARTESIAN_POINT ( 'NONE',  ( 3.455068668934414777, -2.624017327439094327, -3.316620875263732504 ) ) ;
#6996=CARTESIAN_POINT ( 'NONE',  ( 2.500000000000000888, 3.061616997868384127E-16, -4.974599999999998801 ) ) ;
#7007=CARTESIAN_POINT ( 'NONE',  ( 1.144235203016666258, 3.958177651039090250, -0.09382832055445661235 ) ) ;
#7026=DIRECTION ( 'NONE',  ( -0.000000000000000000, -0.000000000000000000, 1.000000000000000000 ) ) ;
#7087=CARTESIAN_POINT ( 'NONE',  ( -4.000000000000000888, -1.539600717839011201, -3.300726591567081591 ) ) ;
#7102=EDGE_CURVE ( 'NONE', #4189, #3920, #1138, .T. ) ;
#7115=EDGE_CURVE ( 'NONE', #10183, #12550, #7539, .T. ) ;
#7118=EDGE_CURVE ( 'NONE', #7909, #6904, #4898, .T. ) ;
#7124=CARTESIAN_POINT ( 'NONE',  ( 4.211405965630455661, 2.460463115436283932, -3.751298928144577882 ) ) ;
#7132=AXIS2_PLACEMENT_3D ( 'NONE', #4586, #3478, #12801 ) ;
#7145=CARTESIAN_POINT ( 'NONE',  ( -4.000000000000000000, 0.8730739991738342143, -3.223134629628428893 ) ) ;
#7149=CLOSED_SHELL ( 'NONE', ( #7407, #2056, #8232, #8754, #4723, #6640, #3726, #2805, #10242, #560, #2886, #4745, #6282, #9227, #11027, #10122, #7592, #3249, #11680, #9620, #12519, #12522, #12180, #10846, #12621, #3167, #9411, #9993, #1338, #2276, #6371, #9386 ) ) ;
#7159=CARTESIAN_POINT ( 'NONE',  ( -4.000000000000000000, -7.806255641895631925E-15, -3.142992957459232350 ) ) ;
#7180=FACE_OUTER_BOUND ( 'NONE', #5222, .T. ) ;
#7197=CARTESIAN_POINT ( 'NONE',  ( -4.000000000000000000, 0.3987449864459974846, -0.01220643443059782861 ) ) ;
#7208=CARTESIAN_POINT ( 'NONE',  ( -2.000000000000006661, 3.464101615137750834, 0.000000000000000000 ) ) ;
#7214=CARTESIAN_POINT ( 'NONE',  ( -3.999999999998910649, -1.658469974638591804, -3.531532913075256186 ) ) ;
#7215=EDGE_CURVE ( 'NONE', #9204, #9576, #8964, .T. ) ;
#7218=EDGE_CURVE ( 'NONE', #10183, #10214, #3784, .T. ) ;
#7220=ORIENTED_EDGE ( 'NONE', *, *, #3661, .F. ) ;
#7258=CARTESIAN_POINT ( 'NONE',  ( 0.000000000000000000, 0.000000000000000000, 0.000000000000000000 ) ) ;
#7267=CARTESIAN_POINT ( 'NONE',  ( 1.567478505476134606E-15, 4.618802153517012066, -3.433295621305382905 ) ) ;
#7278=CARTESIAN_POINT ( 'NONE',  ( 4.235886605889389145, 2.417314728048528760, -3.751161874094018245 ) ) ;
#7281=EDGE_CURVE ( 'NONE', #4712, #2490, #10056, .T. ) ;
#7287=ORIENTED_EDGE ( 'NONE', *, *, #4439, .T. ) ;
#7305=DIRECTION ( 'NONE',  ( 1.224646799147353207E-16, 1.000000000000000000, 0.000000000000000000 ) ) ;
#7310=CARTESIAN_POINT ( 'NONE',  ( -4.000000000000000000, 2.309401076758498483, -0.4999999999999927280 ) ) ;
#7330=DIRECTION ( 'NONE',  ( -1.000000000000000000, 0.000000000000000000, 0.000000000000000000 ) ) ;
#7344=VERTEX_POINT ( 'NONE', #11168 ) ;
#7345=CIRCLE ( 'NONE', #7547, 2.499999999999999556 ) ;
#7355=CARTESIAN_POINT ( 'NONE',  ( -4.000000000000000000, 2.511478553582031203, -3.469254451724764543 ) ) ;
#7359=ORIENTED_EDGE ( 'NONE', *, *, #2118, .F. ) ;
#7377=PLANE ( 'NONE',  #10365 ) ;
#7386=DIRECTION ( 'NONE',  ( -0.5000000000000019984, -0.8660254037844375974, 0.000000000000000000 ) ) ;
#7396=CARTESIAN_POINT ( 'NONE',  ( 1.411581201560190495E-15, 4.862606272033091592, -3.745885042887436622 ) ) ;
#7400=AXIS2_PLACEMENT_3D ( 'NONE', #13156, #3636, #565 ) ;
#7407=ADVANCED_FACE ( 'NONE', ( #6078 ), #12278, .F. ) ;
#7434=AXIS2_PLACEMENT_3D ( 'NONE', #10400, #8267, #8197 ) ;
#7435=CARTESIAN_POINT ( 'NONE',  ( 4.000000000000000000, 2.309401076758497151, -3.433295621305379353 ) ) ;
#7436=CARTESIAN_POINT ( 'NONE',  ( -6.259644161404860030E-16, -4.618802153517027165, -5.000000000000000000 ) ) ;
#7443=DIRECTION ( 'NONE',  ( 0.000000000000000000, 0.000000000000000000, 1.000000000000000000 ) ) ;
#7459=CARTESIAN_POINT ( 'NONE',  ( 0.000000000000000000, 0.000000000000000000, 0.000000000000000000 ) ) ;
#7460=CARTESIAN_POINT ( 'NONE',  ( -2.000000000000006661, 3.464101615137750834, 0.000000000000000000 ) ) ;
#7466=EDGE_CURVE ( 'NONE', #3434, #4810, #6933, .T. ) ;
#7512=CARTESIAN_POINT ( 'NONE',  ( 0.000000000000000000, 0.000000000000000000, -4.484454397937119197 ) ) ;
#7520=ORIENTED_EDGE ( 'NONE', *, *, #7910, .F. ) ;
#7523=CARTESIAN_POINT ( 'NONE',  ( -4.140404888673278272, -2.228338276487456415, -3.686887068327035166 ) ) ;
#7531=FACE_OUTER_BOUND ( 'NONE', #8916, .T. ) ;
#7536=ORIENTED_EDGE ( 'NONE', *, *, #3228, .F. ) ;
#7537=EDGE_LOOP ( 'NONE', ( #5963, #4828, #6802, #4776 ) ) ;
#7539=CIRCLE ( 'NONE', #7980, 5.384454397937118664 ) ;
#7547=AXIS2_PLACEMENT_3D ( 'NONE', #4113, #8337, #9965 ) ;
#7551=VERTEX_POINT ( 'NONE', #5446 ) ;
#7559=DIRECTION ( 'NONE',  ( -1.000000000000000000, 0.000000000000000000, 0.000000000000000000 ) ) ;
#7573=VECTOR ( 'NONE', #4516, 1000.000000000000000 ) ;
#7576=( LENGTH_UNIT ( ) NAMED_UNIT ( * ) SI_UNIT ( .MILLI., .METRE. ) );
#7583=CARTESIAN_POINT ( 'NONE',  ( 2.000000000000008882, 3.464101615137749945, 0.000000000000000000 ) ) ;
#7592=ADVANCED_FACE ( 'NONE', ( #13013 ), #9524, .T. ) ;
#7594=CARTESIAN_POINT ( 'NONE',  ( -3.453038570459499024, -2.625189405340453419, -3.535263753545272891 ) ) ;
#7607=CIRCLE ( 'NONE', #2979, 4.000000000000000000 ) ;
#7641=EDGE_LOOP ( 'NONE', ( #475, #741, #9937, #11617 ) ) ;
#7653=( LENGTH_UNIT ( ) NAMED_UNIT ( * ) SI_UNIT ( .MILLI., .METRE. ) );
#7657=AXIS2_PLACEMENT_3D ( 'NONE', #7985, #700, #9164 ) ;
#7686=VERTEX_POINT ( 'NONE', #12323 ) ;
#7690=DIRECTION ( 'NONE',  ( -0.8660254037844373753, 0.5000000000000021094, 0.000000000000000000 ) ) ;
#7714=CARTESIAN_POINT ( 'NONE',  ( -6.473970235329672780E-16, -4.862606272033106691, -3.745885042887442395 ) ) ;
#7717=B_SPLINE_CURVE_WITH_KNOTS ( 'NONE', 3,
 ( #9750, #9877, #7751, #270, #3663 ),
 .UNSPECIFIED., .F., .F.,
 ( 4, 1, 4 ),
 ( 0.000000000000000000, 0.002309401076758506657, 0.004618802153517013315 ),
 .UNSPECIFIED. ) ;
#7719=B_SPLINE_CURVE_WITH_KNOTS ( 'NONE', 3,
 ( #10816, #374, #12951, #5651, #3496, #1333 ),
 .UNSPECIFIED., .F., .F.,
 ( 4, 2, 4 ),
 ( 4.336808689942017736E-19, 0.0002095117440854729585, 0.0004190234881709454834 ),
 .UNSPECIFIED. ) ;
#7728=CARTESIAN_POINT ( 'NONE',  ( 0.6640947660595348800, -4.471078309994175548, -3.602146406945708090 ) ) ;
#7730=CARTESIAN_POINT ( 'NONE',  ( 5.384454397937118664, 0.000000000000000000, -4.484454397937119197 ) ) ;
#7733=LINE ( 'NONE', #4753, #909 ) ;
#7751=CARTESIAN_POINT ( 'NONE',  ( -1.999999999999999556, 3.464101615137754830, -3.142992957459232795 ) ) ;
#7781=CARTESIAN_POINT ( 'NONE',  ( 0.000000000000000000, 0.000000000000000000, -4.000000000000000000 ) ) ;
#7791=EDGE_LOOP ( 'NONE', ( #2232, #6055, #808 ) ) ;
#7792=ORIENTED_EDGE ( 'NONE', *, *, #1116, .T. ) ;
#7798=CARTESIAN_POINT ( 'NONE',  ( 4.197393957002303999, -0.4069871074557456780, -3.503767560748925813 ) ) ;
#7802=CIRCLE ( 'NONE', #9563, 2.100000000000000089 ) ;
#7811=ORIENTED_EDGE ( 'NONE', *, *, #7218, .F. ) ;
#7815=CARTESIAN_POINT ( 'NONE',  ( 1.734723475976807094E-15, 4.618802153517012954, -0.4999999999999995559 ) ) ;
#7845=CARTESIAN_POINT ( 'NONE',  ( -0.3461262719736137305, 4.658553426539289610, -3.671615880910373608 ) ) ;
#7853=CARTESIAN_POINT ( 'NONE',  ( -5.560781378645575757, 6.809993116116508640E-16, -4.000000000000000000 ) ) ;
#7854=CARTESIAN_POINT ( 'NONE',  ( 2.344047193898588954, 3.265465875126468021, -5.031375706690542042E-16 ) ) ;
#7863=CARTESIAN_POINT ( 'NONE',  ( 4.198928548860774157, -0.8158838809860124996, -3.526471437616918170 ) ) ;
#7878=EDGE_LOOP ( 'NONE', ( #11301, #10334, #279, #9883, #2417, #1318, #12494 ) ) ;
#7909=VERTEX_POINT ( 'NONE', #16 ) ;
#7910=EDGE_CURVE ( 'NONE', #6904, #7909, #12182, .T. ) ;
#7926=CARTESIAN_POINT ( 'NONE',  ( 4.197393957002303999, 7.772902908466098641E-14, -3.503767560748929810 ) ) ;
#7970=EDGE_CURVE ( 'NONE', #5544, #12042, #10357, .T. ) ;
#7975=CARTESIAN_POINT ( 'NONE',  ( 1.828356344711641102, 3.563200125723180900, -5.433716356636336675E-16 ) ) ;
#7980=AXIS2_PLACEMENT_3D ( 'NONE', #1006, #6302, #10496 ) ;
#7985=CARTESIAN_POINT ( 'NONE',  ( 0.000000000000000000, 0.000000000000000000, -5.000000000000000888 ) ) ;
#8031=CARTESIAN_POINT ( 'NONE',  ( 0.000000000000000000, 0.000000000000000000, -0.2800830152838844622 ) ) ;
#8043=CARTESIAN_POINT ( 'NONE',  ( 0.000000000000000000, 0.000000000000000000, 0.000000000000000000 ) ) ;
#8092=CARTESIAN_POINT ( 'NONE',  ( 4.203935335434060505, 1.640780671294165272, -3.598452447879202598 ) ) ;
#8105=CARTESIAN_POINT ( 'NONE',  ( 4.000000000000000000, -2.309401076758514915, -3.433295621305383349 ) ) ;
#8110=CARTESIAN_POINT ( 'NONE',  ( 0.000000000000000000, 0.000000000000000000, 0.000000000000000000 ) ) ;
#8116=CARTESIAN_POINT ( 'NONE',  ( -0.3198814748697807464, -4.434118497892185040, -0.3507732604232532969 ) ) ;
#8133=ORIENTED_EDGE ( 'NONE', *, *, #10083, .T. ) ;
#8176=AXIS2_PLACEMENT_3D ( 'NONE', #11739, #9931, #10830 ) ;
#8182=ORIENTED_EDGE ( 'NONE', *, *, #1875, .T. ) ;
#8197=DIRECTION ( 'NONE',  ( 1.000000000000000000, 0.000000000000000000, 0.000000000000000000 ) ) ;
#8221=ORIENTED_EDGE ( 'NONE', *, *, #12263, .T. ) ;
#8232=ADVANCED_FACE ( 'NONE', ( #11975 ), #9730, .F. ) ;
#8233=CARTESIAN_POINT ( 'NONE',  ( 4.000000000000000000, -2.511475576507276042, -3.469253905236643565 ) ) ;
#8242=DIRECTION ( 'NONE',  ( 0.000000000000000000, 0.000000000000000000, -1.000000000000000000 ) ) ;
#8245=CARTESIAN_POINT ( 'NONE',  ( 4.211140560182196957, 2.431303136016536470, -3.745885042887433514 ) ) ;
#8267=DIRECTION ( 'NONE',  ( -0.000000000000000000, -0.000000000000000000, 1.000000000000000000 ) ) ;
#8295=VERTEX_POINT ( 'NONE', #11060 ) ;
#8297=CARTESIAN_POINT ( 'NONE',  ( -4.000000000000000000, -2.309401076758512694, -3.433295621305382461 ) ) ;
#8301=CARTESIAN_POINT ( 'NONE',  ( -4.000000000000000000, 2.309401076758498483, -0.4999999999999927280 ) ) ;
#8308=EDGE_LOOP ( 'NONE', ( #12632, #4922, #2824 ) ) ;
#8322=AXIS2_PLACEMENT_3D ( 'NONE', #8338, #7305, #10466 ) ;
#8337=DIRECTION ( 'NONE',  ( -0.000000000000000000, -0.000000000000000000, 1.000000000000000000 ) ) ;
#8338=CARTESIAN_POINT ( 'NONE',  ( -5.384454397937118664, 6.594054843588581554E-16, -4.484454397937119197 ) ) ;
#8348=CARTESIAN_POINT ( 'NONE',  ( 1.567478505476134606E-15, 4.618802153517012066, -3.433295621305382905 ) ) ;
#8350=CARTESIAN_POINT ( 'NONE',  ( -4.000000000000000000, -1.560351142792950618, -0.2242961665059814425 ) ) ;
#8357=ORIENTED_EDGE ( 'NONE', *, *, #1116, .F. ) ;
#8379=CARTESIAN_POINT ( 'NONE',  ( 0.6810597143197052450, 4.461075778259290914, -3.598441714920602053 ) ) ;
#8383=AXIS2_PLACEMENT_3D ( 'NONE', #12647, #8242, #952 ) ;
#8384=CARTESIAN_POINT ( 'NONE',  ( 4.000000000000000000, 0.3987449864460005378, -0.01220643443059817035 ) ) ;
#8386=ORIENTED_EDGE ( 'NONE', *, *, #2210, .F. ) ;
#8418=CONICAL_SURFACE ( 'NONE', #4215, 5.560781378645573980, 1.221730476396046816 ) ;
#8419=EDGE_CURVE ( 'NONE', #9288, #4365, #13157, .T. ) ;
#8422=CARTESIAN_POINT ( 'NONE',  ( -4.197393957002303999, -7.773935952363655451E-14, -3.503767560748929810 ) ) ;
#8443=DIRECTION ( 'NONE',  ( -1.000000000000000000, 0.000000000000000000, 0.000000000000000000 ) ) ;
#8448=CONICAL_SURFACE ( 'NONE', #5798, 2.500000000000000888, 0.9599310885968785900 ) ;
#8457=EDGE_CURVE ( 'NONE', #5420, #9576, #5538, .T. ) ;
#8476=EDGE_LOOP ( 'NONE', ( #8182, #11497, #10147, #13503 ) ) ;
#8481=PRESENTATION_STYLE_ASSIGNMENT (( #2171 ) ) ;
#8483=CARTESIAN_POINT ( 'NONE',  ( -3.436319922987618902, 2.634841920961291439, -3.531542292955721862 ) ) ;
#8531=EDGE_CURVE ( 'NONE', #8295, #1117, #1770, .T. ) ;
#8538=B_SPLINE_CURVE_WITH_KNOTS ( 'NONE', 3,
 ( #8297, #12362, #6019, #1990, #10429 ),
 .UNSPECIFIED., .F., .F.,
 ( 4, 1, 4 ),
 ( 0.000000000000000000, 0.002309401076758505356, 0.004618802153517010713 ),
 .UNSPECIFIED. ) ;
#8541=ORIENTED_EDGE ( 'NONE', *, *, #5197, .F. ) ;
#8558=ORIENTED_EDGE ( 'NONE', *, *, #7910, .T. ) ;
#8559=DIRECTION ( 'NONE',  ( -1.000000000000000000, 0.000000000000000000, 0.000000000000000000 ) ) ;
#8561=CARTESIAN_POINT ( 'NONE',  ( 4.000000000000000000, 2.309401076758497151, -3.433295621305379353 ) ) ;
#8568=EDGE_CURVE ( 'NONE', #1304, #13574, #9391, .T. ) ;
#8571=ORIENTED_EDGE ( 'NONE', *, *, #2576, .T. ) ;
#8589=EDGE_CURVE ( 'NONE', #3920, #13411, #8723, .T. ) ;
#8612=( NAMED_UNIT ( * ) PLANE_ANGLE_UNIT ( ) SI_UNIT ( $, .RADIAN. ) );
#8619=CARTESIAN_POINT ( 'NONE',  ( 2.682243648011666703, 3.070208061305304881, -0.04852650426601266831 ) ) ;
#8627=CARTESIAN_POINT ( 'NONE',  ( 4.211140560182196957, 2.431303136016536470, -3.745885042887433514 ) ) ;
#8648=FACE_BOUND ( 'NONE', #133, .T. ) ;
#8656=CONICAL_SURFACE ( 'NONE', #11967, 2.500000000000000888, 0.9599310885968785900 ) ;
#8665=CARTESIAN_POINT ( 'NONE',  ( 2.000000000000005329, -3.464101615137751722, 0.000000000000000000 ) ) ;
#8683=FILL_AREA_STYLE ('',( #2307 ) ) ;
#8716=CARTESIAN_POINT ( 'NONE',  ( -6.259644161404860030E-16, -4.618802153517027165, -3.433295621305388234 ) ) ;
#8723=B_SPLINE_CURVE_WITH_KNOTS ( 'NONE', 3,
 ( #7208, #11413, #1933, #10376, #11487, #7815 ),
 .UNSPECIFIED., .F., .F.,
 ( 4, 2, 4 ),
 ( 0.002365888236227977302, 0.003551327329835078910, 0.004736766423442180518 ),
 .UNSPECIFIED. ) ;
#8744=CARTESIAN_POINT ( 'NONE',  ( 2.548804901056335857E-15, 4.736522675502163437, -3.681124513963624612 ) ) ;
#8754=ADVANCED_FACE ( 'NONE', ( #12028 ), #8418, .T. ) ;
#8763=DIRECTION ( 'NONE',  ( 0.000000000000000000, 0.000000000000000000, -1.000000000000000000 ) ) ;
#8805=ORIENTED_EDGE ( 'NONE', *, *, #8419, .T. ) ;
#8808=CARTESIAN_POINT ( 'NONE',  ( 0.000000000000000000, 0.000000000000000000, 0.000000000000000000 ) ) ;
#8826=ADVANCED_BREP_SHAPE_REPRESENTATION ( '', ( #5714, #430 ), #9487 ) ;
#8830=CARTESIAN_POINT ( 'NONE',  ( -5.384454397937118664, 6.702023979852544604E-16, -5.000000000000000000 ) ) ;
#8841=EDGE_CURVE ( 'NONE', #5652, #5348, #1635, .T. ) ;
#8864=DIRECTION ( 'NONE',  ( 0.5000000000000022204, 0.8660254037844374864, -0.000000000000000000 ) ) ;
#8878=CARTESIAN_POINT ( 'NONE',  ( -3.511755186886750479, 2.826662030176366081, -3.597382984111578086 ) ) ;
#8884=AXIS2_PLACEMENT_3D ( 'NONE', #6682, #2312, #1258 ) ;
#8903=CARTESIAN_POINT ( 'NONE',  ( 2.807080416178989513, -3.225969019225150003, -3.502507215260505014 ) ) ;
#8905=CARTESIAN_POINT ( 'NONE',  ( 2.100000000000000089, 0.000000000000000000, -4.694516984716113228 ) ) ;
#8916=EDGE_LOOP ( 'NONE', ( #9595, #4713, #691 ) ) ;
#8932=ORIENTED_EDGE ( 'NONE', *, *, #9417, .F. ) ;
#8945=CIRCLE ( 'NONE', #9818, 2.500000000000000888 ) ;
#8963=CARTESIAN_POINT ( 'NONE',  ( 4.211140560182196957, -2.431303136016555122, -3.745885042887436622 ) ) ;
#8964=LINE ( 'NONE', #3576, #5337 ) ;
#8994=ORIENTED_EDGE ( 'NONE', *, *, #5197, .T. ) ;
#9033=FACE_OUTER_BOUND ( 'NONE', #11461, .T. ) ;
#9035=CONICAL_SURFACE ( 'NONE', #8383, 4.000000000000000000, 0.8911886515913786111 ) ;
#9052=CARTESIAN_POINT ( 'NONE',  ( 4.204115023516791005, -1.660442669500199919, -3.602151381774560068 ) ) ;
#9056=CARTESIAN_POINT ( 'NONE',  ( -4.101948962585906244, 2.368261337751074169, -3.681124513963621503 ) ) ;
#9057=EDGE_CURVE ( 'NONE', #7909, #9204, #12730, .T. ) ;
#9082=CARTESIAN_POINT ( 'NONE',  ( -0.6448876103708541807, -4.246476118072358474, -0.2256878752776773356 ) ) ;
#9089=CARTESIAN_POINT ( 'NONE',  ( -3.999999999999999112, 1.539600717838996324, -3.300726591567078039 ) ) ;
#9090=CARTESIAN_POINT ( 'NONE',  ( -6.473970235329672780E-16, -4.862606272033106691, -3.745885042887442395 ) ) ;
#9111=CARTESIAN_POINT ( 'NONE',  ( 4.000000000000000000, -2.309401076758514915, -5.000000000000000000 ) ) ;
#9114=( BOUNDED_SURFACE ( )  B_SPLINE_SURFACE ( 3, 2, ( 
 ( #8233, #3722, #2761 ),
 ( #2829, #6840, #9052 ),
 ( #732, #4912, #5882 ),
 ( #13317, #9125, #5054 ),
 ( #3865, #12366, #8092 ),
 ( #12297, #1567, #7124 ) ),
 .UNSPECIFIED., .F., .F., .T. ) 
 B_SPLINE_SURFACE_WITH_KNOTS ( ( 4, 2, 4 ),
 ( 3, 3 ),
 ( 0.02027065861071770947, 0.02273072267836921331, 0.02519078674602071716 ),
 ( 0.000000000000000000, 1.000000000000000000 ),
 .UNSPECIFIED. ) 
 GEOMETRIC_REPRESENTATION_ITEM ( )  RATIONAL_B_SPLINE_SURFACE ( (
 ( 1.000000000000000000, 0.8047781708337304885, 1.000000000000000000),
 ( 1.000000000000000000, 0.8123765190705307671, 1.000000000000000000),
 ( 1.000000000000000000, 0.8190656277163975707, 1.000000000000000000),
 ( 1.000000000000000000, 0.8192366903512159348, 1.000000000000000000),
 ( 1.000000000000000000, 0.8126138454302893610, 1.000000000000000000),
 ( 1.000000000000000000, 0.8047712246031417660, 1.000000000000000000) ) ) 
 REPRESENTATION_ITEM ( '' )  SURFACE ( )  );
#9116=ORIENTED_EDGE ( 'NONE', *, *, #3874, .F. ) ;
#9125=CARTESIAN_POINT ( 'NONE',  ( 4.000000000000000888, 0.8228435280416209752, -3.430609588141487976 ) ) ;
#9128=CARTESIAN_POINT ( 'NONE',  ( -4.197393957002303999, -7.773935952363655451E-14, -3.503767560748929810 ) ) ;
#9139=DIRECTION ( 'NONE',  ( 1.000000000000000000, 0.000000000000000000, 0.000000000000000000 ) ) ;
#9147=FACE_OUTER_BOUND ( 'NONE', #12085, .T. ) ;
#9151=CARTESIAN_POINT ( 'NONE',  ( -1.393927851585477606, 4.043713361053528743, -3.526374918436835149 ) ) ;
#9164=DIRECTION ( 'NONE',  ( -1.000000000000000000, 0.000000000000000000, 0.000000000000000000 ) ) ;
#9170=AXIS2_PLACEMENT_3D ( 'NONE', #11598, #12488, #10347 ) ;
#9195=CARTESIAN_POINT ( 'NONE',  ( -4.197393957002303999, -7.773935952363655451E-14, -3.503767560748929810 ) ) ;
#9204=VERTEX_POINT ( 'NONE', #12032 ) ;
#9210=CARTESIAN_POINT ( 'NONE',  ( 1.999999999999998224, -3.464101615137772594, -3.142992957459239012 ) ) ;
#9227=ADVANCED_FACE ( 'NONE', ( #8648, #2548 ), #3390, .F. ) ;
#9240=EDGE_CURVE ( 'NONE', #3771, #4186, #7717, .T. ) ;
#9243=DIRECTION ( 'NONE',  ( 1.000000000000000000, 0.000000000000000000, 0.000000000000000000 ) ) ;
#9246=CARTESIAN_POINT ( 'NONE',  ( 0.1404048886732821022, 4.699864953788070565, -3.686887068327037387 ) ) ;
#9248=DIRECTION ( 'NONE',  ( 0.8660254037844374864, -0.5000000000000018874, 0.000000000000000000 ) ) ;
#9265=CARTESIAN_POINT ( 'NONE',  ( -4.211140560182196957, 2.431303136016537803, -3.745885042887433514 ) ) ;
#9268=DIRECTION ( 'NONE',  ( 1.000000000000000000, 0.000000000000000000, 0.000000000000000000 ) ) ;
#9279=CARTESIAN_POINT ( 'NONE',  ( 1.274258131564866448, 3.883108878240963513, -3.220599429844046568 ) ) ;
#9288=VERTEX_POINT ( 'NONE', #8716 ) ;
#9309=DIRECTION ( 'NONE',  ( 0.000000000000000000, 0.000000000000000000, 1.000000000000000000 ) ) ;
#9315=CARTESIAN_POINT ( 'NONE',  ( -0.6640947660597427138, 4.471078309994878985, -3.602146406945963442 ) ) ;
#9349=CARTESIAN_POINT ( 'NONE',  ( 0.5449313310647804220, 4.304185902836899835, -3.316620875263383894 ) ) ;
#9368=CARTESIAN_POINT ( 'NONE',  ( 2.500000000000000888, 3.061616997868384127E-16, -4.974599999999998801 ) ) ;
#9386=ADVANCED_FACE ( 'NONE', ( #5954 ), #588, .F. ) ;
#9388=CARTESIAN_POINT ( 'NONE',  ( -4.175648173966055587, 2.207990556236529844, -3.469390959564062626 ) ) ;
#9391=B_SPLINE_CURVE_WITH_KNOTS ( 'NONE', 3,
 ( #8245, #9545, #954, #12515 ),
 .UNSPECIFIED., .F., .F.,
 ( 4, 4 ),
 ( 0.000000000000000000, 0.002452478801916361129 ),
 .UNSPECIFIED. ) ;
#9411=ADVANCED_FACE ( 'NONE', ( #12227 ), #9114, .F. ) ;
#9417=EDGE_CURVE ( 'NONE', #4712, #6427, #9773, .T. ) ;
#9458=DIRECTION ( 'NONE',  ( -0.000000000000000000, -0.000000000000000000, 1.000000000000000000 ) ) ;
#9487=( GEOMETRIC_REPRESENTATION_CONTEXT ( 3 ) GLOBAL_UNCERTAINTY_ASSIGNED_CONTEXT ( ( #11862 ) ) GLOBAL_UNIT_ASSIGNED_CONTEXT ( ( #5506, #8612, #11716 ) ) REPRESENTATION_CONTEXT ( 'NONE', 'WORKASPACE' ) );
#9524=CONICAL_SURFACE ( 'NONE', #6240, 5.560781378645573980, 1.221730476396046816 ) ;
#9545=CARTESIAN_POINT ( 'NONE',  ( 4.203833317240879275, 1.627343821129582979, -3.597273115243889929 ) ) ;
#9559=EDGE_CURVE ( 'NONE', #4810, #4189, #2663, .T. ) ;
#9563=AXIS2_PLACEMENT_3D ( 'NONE', #2972, #12506, #661 ) ;
#9576=VERTEX_POINT ( 'NONE', #12573 ) ;
#9595=ORIENTED_EDGE ( 'NONE', *, *, #6018, .T. ) ;
#9599=CARTESIAN_POINT ( 'NONE',  ( -4.000000000000000000, 2.309401076758498483, -0.4999999999999927280 ) ) ;
#9620=ADVANCED_FACE ( 'NONE', ( #7531 ), #3753, .T. ) ;
#9636=( BOUNDED_SURFACE ( )  B_SPLINE_SURFACE ( 3, 2, ( 
 ( #3575, #11935, #2454 ),
 ( #12074, #11025, #7728 ),
 ( #444, #12140, #1409 ),
 ( #5656, #10127, #8903 ),
 ( #6962, #9990, #2662 ),
 ( #11167, #6890, #4612 ) ),
 .UNSPECIFIED., .F., .F., .F. ) 
 B_SPLINE_SURFACE_WITH_KNOTS ( ( 4, 2, 4 ),
 ( 3, 3 ),
 ( 0.02032853247518126918, 0.02278863295364821906, 0.02524873343211517240 ),
 ( 0.000000000000000000, 1.000000000000000000 ),
 .UNSPECIFIED. ) 
 GEOMETRIC_REPRESENTATION_ITEM ( )  RATIONAL_B_SPLINE_SURFACE ( (
 ( 1.000000000000000000, 0.8047781615896837382, 1.000000000000000000),
 ( 1.000000000000000000, 0.8123767586289252218, 1.000000000000000000),
 ( 1.000000000000000000, 0.8190662415564388121, 1.000000000000000000),
 ( 1.000000000000000000, 0.8192361015669026303, 1.000000000000000000),
 ( 1.000000000000000000, 0.8126135807103900266, 1.000000000000000000),
 ( 1.000000000000000000, 0.8047712338318593339, 1.000000000000000000) ) ) 
 REPRESENTATION_ITEM ( '' )  SURFACE ( )  );
#9690=CARTESIAN_POINT ( 'NONE',  ( 2.500000000000000444, 0.000000000000000000, -25.03750572909317285 ) ) ;
#9708=ORIENTED_EDGE ( 'NONE', *, *, #7466, .T. ) ;
#9722=( NAMED_UNIT ( * ) PLANE_ANGLE_UNIT ( ) SI_UNIT ( $, .RADIAN. ) );
#9730=CONICAL_SURFACE ( 'NONE', #2651, 2.059999999999998721, 0.9599310885968738161 ) ;
#9733=CARTESIAN_POINT ( 'NONE',  ( 0.000000000000000000, 0.000000000000000000, -4.694516984716113228 ) ) ;
#9750=CARTESIAN_POINT ( 'NONE',  ( 1.567478505476134606E-15, 4.618802153517012066, -3.433295621305382905 ) ) ;
#9773=B_SPLINE_CURVE_WITH_KNOTS ( 'NONE', 3,
 ( #9195, #4771, #10011, #528, #13389, #9265 ),
 .UNSPECIFIED., .F., .F.,
 ( 4, 2, 4 ),
 ( 0.002452478801916376308, 0.003676905084148007850, 0.004901331366379639391 ),
 .UNSPECIFIED. ) ;
#9790=EDGE_LOOP ( 'NONE', ( #4485, #4609, #4764, #330, #1358 ) ) ;
#9818=AXIS2_PLACEMENT_3D ( 'NONE', #12568, #6161, #10358 ) ;
#9821=CARTESIAN_POINT ( 'NONE',  ( -4.000000000000000000, -2.309401076758515803, -0.4999999999999995559 ) ) ;
#9829=ORIENTED_EDGE ( 'NONE', *, *, #11221, .T. ) ;
#9853=CARTESIAN_POINT ( 'NONE',  ( 4.000000000000000000, 2.309401076758515803, -0.4999999999999995559 ) ) ;
#9868=CARTESIAN_POINT ( 'NONE',  ( 4.000000000000000000, 2.309401076758497151, -3.433295621305379353 ) ) ;
#9877=CARTESIAN_POINT ( 'NONE',  ( -0.6666666666666651864, 4.233901974057260098, -3.300726591567081147 ) ) ;
#9883=ORIENTED_EDGE ( 'NONE', *, *, #7281, .F. ) ;
#9889=CARTESIAN_POINT ( 'NONE',  ( 4.000000000000000000, 0.000000000000000000, 0.000000000000000000 ) ) ;
#9931=DIRECTION ( 'NONE',  ( 0.000000000000000000, 0.000000000000000000, -1.000000000000000000 ) ) ;
#9937=ORIENTED_EDGE ( 'NONE', *, *, #5940, .T. ) ;
#9953=AXIS2_PLACEMENT_3D ( 'NONE', #10341, #7026, #9243 ) ;
#9955=ORIENTED_EDGE ( 'NONE', *, *, #832, .F. ) ;
#9965=DIRECTION ( 'NONE',  ( 1.000000000000000000, 0.000000000000000000, 0.000000000000000000 ) ) ;
#9990=CARTESIAN_POINT ( 'NONE',  ( 3.436319922986518449, -2.634841920959471562, -3.531542292954761741 ) ) ;
#9993=ADVANCED_FACE ( 'NONE', ( #13583 ), #1493, .F. ) ;
#10007=B_SPLINE_CURVE_WITH_KNOTS ( 'NONE', 3,
 ( #5440, #3550, #8744, #6477, #10679, #5499 ),
 .UNSPECIFIED., .F., .F.,
 ( 4, 2, 4 ),
 ( -3.640115492407174633E-06, 0.0002066546034006553863, 0.0004169493222937179812 ),
 .UNSPECIFIED. ) ;
#10011=CARTESIAN_POINT ( 'NONE',  ( -4.198928548860774157, 0.8158838809860065044, -3.526471437616918170 ) ) ;
#10019=ORIENTED_EDGE ( 'NONE', *, *, #12581, .T. ) ;
#10038=DIRECTION ( 'NONE',  ( -0.000000000000000000, 0.000000000000000000, -1.000000000000000000 ) ) ;
#10055=CARTESIAN_POINT ( 'NONE',  ( 2.687328764639642653, -3.067272167851299969, -0.05923475698271395140 ) ) ;
#10056=LINE ( 'NONE', #571, #11953 ) ;
#10083=EDGE_CURVE ( 'NONE', #6658, #2470, #3996, .T. ) ;
#10108=CARTESIAN_POINT ( 'NONE',  ( 1.734723475976807094E-15, 4.618802153517012954, -0.4999999999999995559 ) ) ;
#10122=ADVANCED_FACE ( 'NONE', ( #2441 ), #5759, .T. ) ;
#10127=CARTESIAN_POINT ( 'NONE',  ( 2.712762565639649015, -3.052587955997662306, -3.430618716626630871 ) ) ;
#10147=ORIENTED_EDGE ( 'NONE', *, *, #687, .T. ) ;
#10163=APPLICATION_CONTEXT ( 'automotive_design' ) ;
#10182=CARTESIAN_POINT ( 'NONE',  ( -4.211140560182196957, 2.431303136016537803, -3.745885042887433514 ) ) ;
#10183=VERTEX_POINT ( 'NONE', #13623 ) ;
#10201=ORIENTED_EDGE ( 'NONE', *, *, #11339, .F. ) ;
#10204=CARTESIAN_POINT ( 'NONE',  ( -2.500000000000000888, 0.000000000000000000, -4.974599999999998801 ) ) ;
#10214=VERTEX_POINT ( 'NONE', #3129 ) ;
#10219=ORIENTED_EDGE ( 'NONE', *, *, #7466, .F. ) ;
#10241=CARTESIAN_POINT ( 'NONE',  ( -4.000000000000000000, 1.700094919196744270, -3.320312364301766017 ) ) ;
#10242=ADVANCED_FACE ( 'NONE', ( #2281 ), #11974, .T. ) ;
#10246=VERTEX_POINT ( 'NONE', #9889 ) ;
#10270=ORIENTED_EDGE ( 'NONE', *, *, #5203, .T. ) ;
#10274=CONICAL_SURFACE ( 'NONE', #11787, 4.000000000000000000, 0.8911886515913786111 ) ;
#10297=CARTESIAN_POINT ( 'NONE',  ( 0.000000000000000000, 0.000000000000000000, -5.000000000000000000 ) ) ;
#10314=EDGE_LOOP ( 'NONE', ( #2213, #5943, #10270, #5983 ) ) ;
#10316=ORIENTED_EDGE ( 'NONE', *, *, #3320, .T. ) ;
#10330=FACE_OUTER_BOUND ( 'NONE', #5653, .T. ) ;
#10334=ORIENTED_EDGE ( 'NONE', *, *, #5526, .T. ) ;
#10335=DIRECTION ( 'NONE',  ( 0.000000000000000000, 0.000000000000000000, 1.000000000000000000 ) ) ;
#10341=CARTESIAN_POINT ( 'NONE',  ( 0.000000000000000000, 0.000000000000000000, -25.03750572909317285 ) ) ;
#10347=DIRECTION ( 'NONE',  ( 1.000000000000000000, 0.000000000000000000, 0.000000000000000000 ) ) ;
#10353=STYLED_ITEM('',(#13712),#5714);
#10357=B_SPLINE_CURVE_WITH_KNOTS ( 'NONE', 3,
 ( #5355, #2089, #1105, #6463, #4238, #3063 ),
 .UNSPECIFIED., .F., .F.,
 ( 4, 2, 4 ),
 ( -3.640115492409406142E-06, 0.0002066546034006526487, 0.0004169493222937146744 ),
 .UNSPECIFIED. ) ;
#10358=DIRECTION ( 'NONE',  ( 1.000000000000000000, 0.000000000000000000, 0.000000000000000000 ) ) ;
#10365=AXIS2_PLACEMENT_3D ( 'NONE', #6212, #12676, #10335 ) ;
#10370=AXIS2_PLACEMENT_3D ( 'NONE', #204, #4426, #11957 ) ;
#10376=CARTESIAN_POINT ( 'NONE',  ( -0.6507732100473471171, 4.243078065514775510, -0.2236248678334823436 ) ) ;
#10377=STYLED_ITEM ( 'NONE', ( #8481 ), #8826 ) ;
#10381=FACE_OUTER_BOUND ( 'NONE', #10819, .T. ) ;
#10384=ORIENTED_EDGE ( 'NONE', *, *, #3665, .T. ) ;
#10390=CARTESIAN_POINT ( 'NONE',  ( -6.259644161404862988E-16, -4.618802153517027165, -3.504271511726793076 ) ) ;
#10399=LINE ( 'NONE', #9368, #10851 ) ;
#10400=CARTESIAN_POINT ( 'NONE',  ( 0.000000000000000000, 0.000000000000000000, -5.000000000000000000 ) ) ;
#10421=EDGE_LOOP ( 'NONE', ( #2541, #6752 ) ) ;
#10429=CARTESIAN_POINT ( 'NONE',  ( -6.259644161404860030E-16, -4.618802153517027165, -3.433295621305388234 ) ) ;
#10440=ORIENTED_EDGE ( 'NONE', *, *, #1875, .F. ) ;
#10441=ORIENTED_EDGE ( 'NONE', *, *, #7102, .F. ) ;
#10466=DIRECTION ( 'NONE',  ( -1.000000000000000000, 1.224646799147352714E-16, 0.000000000000000000 ) ) ;
#10475=CIRCLE ( 'NONE', #7400, 4.000000000000000000 ) ;
#10490=B_SPLINE_CURVE_WITH_KNOTS ( 'NONE', 3,
 ( #12957, #509, #10960, #10890, #10055, #4749, #13096, #13227 ),
 .UNSPECIFIED., .F., .F.,
 ( 4, 2, 2, 4 ),
 ( 2.465131517071610173E-07, 0.001183067374689837636, 0.001774477805458902699, 0.002365888236227967761 ),
 .UNSPECIFIED. ) ;
#10496=DIRECTION ( 'NONE',  ( 1.000000000000000000, 0.000000000000000000, 0.000000000000000000 ) ) ;
#10517=CARTESIAN_POINT ( 'NONE',  ( 4.000000000000000000, 0.1981133338132474442, 2.382280164152719704E-17 ) ) ;
#10520=ORIENTED_EDGE ( 'NONE', *, *, #2758, .F. ) ;
#10524=ORIENTED_EDGE ( 'NONE', *, *, #11339, .T. ) ;
#10546=SHAPE_REPRESENTATION_RELATIONSHIP ( 'NONE' , 'NONE' ,  #180, #8826 ) ;
#10548=CARTESIAN_POINT ( 'NONE',  ( 0.02448733951239481094, 4.877042772274728044, -3.751161874094022242 ) ) ;
#10557=CARTESIAN_POINT ( 'NONE',  ( 0.02511973781850649831, -4.877415612947427981, -3.751298745799844792 ) ) ;
#10592=MECHANICAL_DESIGN_GEOMETRIC_PRESENTATION_REPRESENTATION('',(#10377),#6626);
#10604=LINE ( 'NONE', #226, #7573 ) ;
#10629=CARTESIAN_POINT ( 'NONE',  ( -3.540020015735593439, -2.810662092924100630, -3.602146406945814672 ) ) ;
#10630=FACE_OUTER_BOUND ( 'NONE', #7791, .T. ) ;
#10646=ORIENTED_EDGE ( 'NONE', *, *, #5049, .T. ) ;
#10664=CARTESIAN_POINT ( 'NONE',  ( 4.197393957002303999, 7.772902908466098641E-14, -3.503767560748929810 ) ) ;
#10679=CARTESIAN_POINT ( 'NONE',  ( 1.567478505476135000E-15, 4.618802153517012954, -3.504269196027527844 ) ) ;
#10694=ORIENTED_EDGE ( 'NONE', *, *, #4439, .F. ) ;
#10701=CARTESIAN_POINT ( 'NONE',  ( -2.855764796983342624, 2.970025579236414082, -0.09382832055445475272 ) ) ;
#10718=DIRECTION ( 'NONE',  ( -1.000000000000000000, 0.000000000000000000, 0.000000000000000000 ) ) ;
#10727=DIRECTION ( 'NONE',  ( 1.000000000000000000, 0.000000000000000000, 0.000000000000000000 ) ) ;
#10734=DIRECTION ( 'NONE',  ( 0.5000000000000013323, -0.8660254037844379305, 0.000000000000000000 ) ) ;
#10738=EDGE_LOOP ( 'NONE', ( #3653, #12191, #4340, #10440, #4939 ) ) ;
#10741=ORIENTED_EDGE ( 'NONE', *, *, #8841, .T. ) ;
#10757=ORIENTED_EDGE ( 'NONE', *, *, #832, .T. ) ;
#10787=CARTESIAN_POINT ( 'NONE',  ( 4.000000000000000000, 2.309401076758497151, -5.000000000000000000 ) ) ;
#10804=CARTESIAN_POINT ( 'NONE',  ( -1.391697335622809950, -4.043246145443391448, -3.503898532754372575 ) ) ;
#10816=CARTESIAN_POINT ( 'NONE',  ( 4.000000000000000000, -2.309401076758514915, -3.433295621305383349 ) ) ;
#10819=EDGE_LOOP ( 'NONE', ( #596, #12105, #11, #8932, #13191 ) ) ;
#10827=CARTESIAN_POINT ( 'NONE',  ( 3.999999999999999112, 2.309401076758497595, -3.504271511726784194 ) ) ;
#10830=DIRECTION ( 'NONE',  ( -1.000000000000000000, 0.000000000000000000, 0.000000000000000000 ) ) ;
#10841=AXIS2_PLACEMENT_3D ( 'NONE', #7730, #13097, #13162 ) ;
#10846=ADVANCED_FACE ( 'NONE', ( #3302 ), #11498, .F. ) ;
#10851=VECTOR ( 'NONE', #13567, 1000.000000000000114 ) ;
#10853=ORIENTED_EDGE ( 'NONE', *, *, #9559, .T. ) ;
#10890=CARTESIAN_POINT ( 'NONE',  ( 2.855764796983346177, -2.970025579236428737, -0.09382832055446485575 ) ) ;
#10924=ORIENTED_EDGE ( 'NONE', *, *, #99, .F. ) ;
#10960=CARTESIAN_POINT ( 'NONE',  ( 3.355112389629172576, -2.681727112203168950, -0.2256878752776777242 ) ) ;
#10963=DIRECTION ( 'NONE',  ( 0.000000000000000000, 0.000000000000000000, -1.000000000000000000 ) ) ;
#10989=B_SPLINE_CURVE_WITH_KNOTS ( 'NONE', 3,
 ( #12306, #671, #10804, #4924, #13329, #3484, #11271, #6040 ),
 .UNSPECIFIED., .F., .F.,
 ( 4, 2, 2, 4 ),
 ( 0.000000000000000000, 0.002450665683189818828, 0.003675998524784728459, 0.004901331366379638524 ),
 .UNSPECIFIED. ) ;
#10990=DIRECTION ( 'NONE',  ( 0.000000000000000000, 0.000000000000000000, 1.000000000000000000 ) ) ;
#11020=DIRECTION ( 'NONE',  ( -0.000000000000000000, -0.000000000000000000, 1.000000000000000000 ) ) ;
#11024=FACE_OUTER_BOUND ( 'NONE', #11423, .T. ) ;
#11025=CARTESIAN_POINT ( 'NONE',  ( 0.5469614295415388128, -4.303013824935362663, -3.535263753543555598 ) ) ;
#11027=ADVANCED_FACE ( 'NONE', ( #11932, #11024 ), #1543, .T. ) ;
#11030=DIRECTION ( 'NONE',  ( -1.000000000000000000, 0.000000000000000000, 0.000000000000000000 ) ) ;
#11051=CARTESIAN_POINT ( 'NONE',  ( -4.154094228333456762, 2.398367420968013253, -3.721909803043220055 ) ) ;
#11060=CARTESIAN_POINT ( 'NONE',  ( 2.000000000000005329, -3.464101615137751722, 0.000000000000000000 ) ) ;
#11072=CARTESIAN_POINT ( 'NONE',  ( -1.312671235360383548, -3.860931062424228788, -0.05923475698271369466 ) ) ;
#11123=ORIENTED_EDGE ( 'NONE', *, *, #5211, .T. ) ;
#11132=DIRECTION ( 'NONE',  ( 1.000000000000000000, 0.000000000000000000, 0.000000000000000000 ) ) ;
#11133=CARTESIAN_POINT ( 'NONE',  ( 0.6666666666666658525, -4.233901974057276085, -3.300726591567086476 ) ) ;
#11137=AXIS2_PLACEMENT_3D ( 'NONE', #1909, #7386, #9248 ) ;
#11163=EDGE_CURVE ( 'NONE', #4186, #4189, #3978, .T. ) ;
#11167=CARTESIAN_POINT ( 'NONE',  ( 4.175648173966055587, -2.207990556236547608, -3.469390959564065291 ) ) ;
#11168=CARTESIAN_POINT ( 'NONE',  ( 1.411581201560190495E-15, 4.862606272033091592, -3.745885042887436622 ) ) ;
#11213=CARTESIAN_POINT ( 'NONE',  ( 1.312671235360372224, 3.860931062424219462, -0.05923475698270440348 ) ) ;
#11221=EDGE_CURVE ( 'NONE', #5652, #3771, #1760, .T. ) ;
#11223=MECHANICAL_DESIGN_GEOMETRIC_PRESENTATION_REPRESENTATION('',(#10353),#13202);
#11271=CARTESIAN_POINT ( 'NONE',  ( -3.861362476283256129, -2.629030857716004199, -3.671615880910374941 ) ) ;
#11301=ORIENTED_EDGE ( 'NONE', *, *, #8568, .T. ) ;
#11302=CIRCLE ( 'NONE', #2472, 2.100000000000000089 ) ;
#11328=CARTESIAN_POINT ( 'NONE',  ( 0.000000000000000000, 0.000000000000000000, -25.03750572909317285 ) ) ;
#11334=EDGE_CURVE ( 'NONE', #3771, #13411, #11525, .T. ) ;
#11338=B_SPLINE_CURVE_WITH_KNOTS ( 'NONE', 3,
 ( #6049, #10517, #8384, #5147, #13549, #12591, #4099, #4934 ),
 .UNSPECIFIED., .F., .F.,
 ( 4, 2, 2, 4 ),
 ( 0.005725059856848645212, 0.006314084072593634418, 0.006903108288338624492, 0.008081156719828603771 ),
 .UNSPECIFIED. ) ;
#11339=EDGE_CURVE ( 'NONE', #6904, #11968, #3221, .T. ) ;
#11361=CARTESIAN_POINT ( 'NONE',  ( -1.240299975428113101E-15, -4.647091401871173311, -3.572172305156514849 ) ) ;
#11399=AXIS2_PLACEMENT_3D ( 'NONE', #5434, #357, #6667 ) ;
#11402=CARTESIAN_POINT ( 'NONE',  ( -4.000000000000000000, 0.7924765000094600165, -0.05906175389889745803 ) ) ;
#11413=CARTESIAN_POINT ( 'NONE',  ( -1.655952806101422814, 3.662737355149034979, -7.623296525288699970E-18 ) ) ;
#11423=EDGE_LOOP ( 'NONE', ( #537, #6263 ) ) ;
#11461=EDGE_LOOP ( 'NONE', ( #12138, #8994, #6249, #13538 ) ) ;
#11474=EDGE_CURVE ( 'NONE', #10246, #8295, #4396, .T. ) ;
#11476=LINE ( 'NONE', #1658, #2462 ) ;
#11487=CARTESIAN_POINT ( 'NONE',  ( -0.3208286057739654917, 4.433571671609680465, -0.3503314178412548774 ) ) ;
#11489=CARTESIAN_POINT ( 'NONE',  ( 3.472371940585993855, 2.614027278893175321, -3.320322319201766792 ) ) ;
#11494=CARTESIAN_POINT ( 'NONE',  ( -4.000000000000000000, -0.8232339106130515116, -3.430630286862743183 ) ) ;
#11497=ORIENTED_EDGE ( 'NONE', *, *, #12407, .F. ) ;
#11498=( BOUNDED_SURFACE ( )  B_SPLINE_SURFACE ( 3, 2, ( 
 ( #1269, #7523, #11606 ),
 ( #2250, #7594, #10629 ),
 ( #2184, #12633, #6429 ),
 ( #12826, #119, #5319 ),
 ( #1068, #11798, #5255 ),
 ( #5517, #248, #10557 ) ),
 .UNSPECIFIED., .F., .F., .F. ) 
 B_SPLINE_SURFACE_WITH_KNOTS ( ( 4, 2, 4 ),
 ( 3, 3 ),
 ( 0.02032853247518126918, 0.02278863295364821906, 0.02524873343211516893 ),
 ( 0.000000000000000000, 1.000000000000000000 ),
 .UNSPECIFIED. ) 
 GEOMETRIC_REPRESENTATION_ITEM ( )  RATIONAL_B_SPLINE_SURFACE ( (
 ( 1.000000000000000000, 0.8047781615896838492, 1.000000000000000000),
 ( 1.000000000000000000, 0.8123767586288186404, 1.000000000000000000),
 ( 1.000000000000000000, 0.8190662415565814758, 1.000000000000000000),
 ( 1.000000000000000000, 0.8192361015667604107, 1.000000000000000000),
 ( 1.000000000000000000, 0.8126135807104967190, 1.000000000000000000),
 ( 1.000000000000000000, 0.8047712338318580017, 1.000000000000000000) ) ) 
 REPRESENTATION_ITEM ( '' )  SURFACE ( )  );
#11525=LINE ( 'NONE', #2166, #6401 ) ;
#11526=AXIS2_PLACEMENT_3D ( 'NONE', #9733, #9458, #11663 ) ;
#11553=EDGE_LOOP ( 'NONE', ( #868, #9955, #8357 ) ) ;
#11556=EDGE_CURVE ( 'NONE', #2470, #5544, #10989, .T. ) ;
#11562=CARTESIAN_POINT ( 'NONE',  ( 4.175002511812151873, 2.208363329454889445, -3.469254087858244073 ) ) ;
#11566=CARTESIAN_POINT ( 'NONE',  ( -4.000000000000000000, 2.471528634177585282, -3.686887442155186712 ) ) ;
#11574=CARTESIAN_POINT ( 'NONE',  ( 0.000000000000000000, 0.000000000000000000, -4.694516984716113228 ) ) ;
#11589=ORIENTED_EDGE ( 'NONE', *, *, #11556, .F. ) ;
#11590=DIRECTION ( 'NONE',  ( 0.000000000000000000, 0.000000000000000000, 1.000000000000000000 ) ) ;
#11591=DIRECTION ( 'NONE',  ( -0.8191520442889902442, 0.000000000000000000, -0.5735764363510482688 ) ) ;
#11598=CARTESIAN_POINT ( 'NONE',  ( 0.000000000000000000, 0.000000000000000000, -4.484454397937119197 ) ) ;
#11599=VECTOR ( 'NONE', #13306, 1000.000000000000000 ) ;
#11606=CARTESIAN_POINT ( 'NONE',  ( -4.235886605889389145, -2.417314728048544303, -3.751161874094020909 ) ) ;
#11617=ORIENTED_EDGE ( 'NONE', *, *, #8457, .T. ) ;
#11647=ORIENTED_EDGE ( 'NONE', *, *, #284, .T. ) ;
#11651=CARTESIAN_POINT ( 'NONE',  ( -4.000000000000000000, -0.3979232138631226823, -3.896351557369779711E-17 ) ) ;
#11660=ORIENTED_EDGE ( 'NONE', *, *, #12917, .T. ) ;
#11662=DIRECTION ( 'NONE',  ( -1.000000000000000000, 0.000000000000000000, 0.000000000000000000 ) ) ;
#11663=DIRECTION ( 'NONE',  ( -1.000000000000000000, 0.000000000000000000, 0.000000000000000000 ) ) ;
#11680=ADVANCED_FACE ( 'NONE', ( #4994 ), #9035, .T. ) ;
#11701=B_SPLINE_CURVE_WITH_KNOTS ( 'NONE', 3,
 ( #8561, #10827, #124, #12961, #4547, #1343 ),
 .UNSPECIFIED., .F., .F.,
 ( 4, 2, 4 ),
 ( 0.000000000000000000, 0.0002095117440854730670, 0.0004190234881709461339 ),
 .UNSPECIFIED. ) ;
#11703=FACE_OUTER_BOUND ( 'NONE', #5350, .T. ) ;
#11716=( NAMED_UNIT ( * ) SI_UNIT ( $, .STERADIAN. ) SOLID_ANGLE_UNIT ( ) );
#11722=CARTESIAN_POINT ( 'NONE',  ( 4.000000000000000000, -2.309401076758516691, -0.4999999999999995559 ) ) ;
#11739=CARTESIAN_POINT ( 'NONE',  ( 0.000000000000000000, 0.000000000000000000, 0.000000000000000000 ) ) ;
#11785=DIRECTION ( 'NONE',  ( -0.000000000000000000, -0.000000000000000000, 1.000000000000000000 ) ) ;
#11787=AXIS2_PLACEMENT_3D ( 'NONE', #7459, #8763, #11662 ) ;
#11798=CARTESIAN_POINT ( 'NONE',  ( -0.5636800770129166693, -4.293361309317430319, -3.531542292955206275 ) ) ;
#11851=SURFACE_SIDE_STYLE ('',( #3423 ) ) ;
#11854=CARTESIAN_POINT ( 'NONE',  ( 1.747541505913279281, -3.837784562140273081, -3.503702292528912299 ) ) ;
#11862=UNCERTAINTY_MEASURE_WITH_UNIT (LENGTH_MEASURE( 1.000000000000000082E-05 ), #5506, 'distance_accuracy_value', 'NONE');
#11912=ORIENTED_EDGE ( 'NONE', *, *, #12482, .T. ) ;
#11931=ORIENTED_EDGE ( 'NONE', *, *, #7218, .T. ) ;
#11932=FACE_BOUND ( 'NONE', #10421, .T. ) ;
#11935=CARTESIAN_POINT ( 'NONE',  ( -0.1404048886732797152, -4.699864953788083888, -3.686887068327043160 ) ) ;
#11953=VECTOR ( 'NONE', #5657, 1000.000000000000227 ) ;
#11957=DIRECTION ( 'NONE',  ( -1.000000000000000000, 0.000000000000000000, 0.000000000000000000 ) ) ;
#11963=AXIS2_PLACEMENT_3D ( 'NONE', #11574, #12794, #7559 ) ;
#11967=AXIS2_PLACEMENT_3D ( 'NONE', #6823, #10963, #11030 ) ;
#11968=VERTEX_POINT ( 'NONE', #5535 ) ;
#11974=PLANE ( 'NONE',  #820 ) ;
#11975=FACE_OUTER_BOUND ( 'NONE', #10314, .T. ) ;
#11976=CARTESIAN_POINT ( 'NONE',  ( -2.688821387764050996E-14, -4.618802153517012954, -0.4999999999999995559 ) ) ;
#11988=DIRECTION ( 'NONE',  ( -0.000000000000000000, 0.000000000000000000, -1.000000000000000000 ) ) ;
#12002=B_SPLINE_CURVE_WITH_KNOTS ( 'NONE', 3,
 ( #10182, #8878, #422, #688, #9151, #4658, #7845, #2645 ),
 .UNSPECIFIED., .F., .F.,
 ( 4, 2, 2, 4 ),
 ( 0.000000000000000000, 0.002450665683189820997, 0.003675998524784731495, 0.004901331366379641993 ),
 .UNSPECIFIED. ) ;
#12028=FACE_OUTER_BOUND ( 'NONE', #7878, .T. ) ;
#12032=CARTESIAN_POINT ( 'NONE',  ( -2.100000000000000089, 2.571758278209441957E-16, -0.2800830152838844622 ) ) ;
#12042=VERTEX_POINT ( 'NONE', #1490 ) ;
#12052=B_SPLINE_CURVE_WITH_KNOTS ( 'NONE', 3,
 ( #11722, #6488, #5110, #13586, #4133, #3494 ),
 .UNSPECIFIED., .F., .F.,
 ( 4, 2, 4 ),
 ( 0.003358874760055551890, 0.004541967308452098118, 0.005725059856848645212 ),
 .UNSPECIFIED. ) ;
#12059=CIRCLE ( 'NONE', #11399, 2.500000000000000444 ) ;
#12065=CARTESIAN_POINT ( 'NONE',  ( 3.679171394226031122, 2.494631558665830973, -0.3503314178412474389 ) ) ;
#12074=CARTESIAN_POINT ( 'NONE',  ( 0.5276280594147412240, -4.314175951381924889, -3.320322319201654881 ) ) ;
#12075=DIRECTION ( 'NONE',  ( -0.8191520442889875797, 1.003171929053519570E-16, 0.5735764363510522656 ) ) ;
#12085=EDGE_LOOP ( 'NONE', ( #3096, #10219, #2132 ) ) ;
#12105=ORIENTED_EDGE ( 'NONE', *, *, #4935, .F. ) ;
#12123=DIRECTION ( 'NONE',  ( -1.000000000000000000, 0.000000000000000000, 0.000000000000000000 ) ) ;
#12138=ORIENTED_EDGE ( 'NONE', *, *, #7118, .T. ) ;
#12140=CARTESIAN_POINT ( 'NONE',  ( 1.257172072275274388, -3.892973519170983110, -3.433252694550781303 ) ) ;
#12148=CARTESIAN_POINT ( 'NONE',  ( 4.000000000000000000, -2.309401076758516691, -0.4999999999999995559 ) ) ;
#12180=ADVANCED_FACE ( 'NONE', ( #3861 ), #3415, .T. ) ;
#12182=CIRCLE ( 'NONE', #11963, 2.100000000000000089 ) ;
#12190=CARTESIAN_POINT ( 'NONE',  ( 2.000000000000008882, 3.464101615137749945, 0.000000000000000000 ) ) ;
#12191=ORIENTED_EDGE ( 'NONE', *, *, #12581, .F. ) ;
#12203=CONICAL_SURFACE ( 'NONE', #13514, 4.000000000000000000, 0.8911886515913786111 ) ;
#12227=FACE_OUTER_BOUND ( 'NONE', #10738, .T. ) ;
#12230=CARTESIAN_POINT ( 'NONE',  ( -4.000000000000004441, 2.309401076758496263, -3.504269196027523847 ) ) ;
#12253=VECTOR ( 'NONE', #249, 1000.000000000000000 ) ;
#12256=CARTESIAN_POINT ( 'NONE',  ( -2.000000000000007550, -3.464101615137749945, 0.000000000000000000 ) ) ;
#12263=EDGE_CURVE ( 'NONE', #12042, #9288, #8538, .T. ) ;
#12278=CYLINDRICAL_SURFACE ( 'NONE', #9953, 2.500000000000000444 ) ;
#12297=CARTESIAN_POINT ( 'NONE',  ( 4.000000000000000000, 2.512223110932545023, -3.469391141908803711 ) ) ;
#12306=CARTESIAN_POINT ( 'NONE',  ( -6.473970235329672780E-16, -4.862606272033106691, -3.745885042887442395 ) ) ;
#12308=CARTESIAN_POINT ( 'NONE',  ( 0.000000000000000000, 0.000000000000000000, -5.000000000000000000 ) ) ;
#12310=B_SPLINE_CURVE_WITH_KNOTS ( 'NONE', 3,
 ( #13534, #805, #4916, #9128 ),
 .UNSPECIFIED., .F., .F.,
 ( 4, 4 ),
 ( 0.000000000000000000, 0.002452478801916376308 ),
 .UNSPECIFIED. ) ;
#12314=CARTESIAN_POINT ( 'NONE',  ( -4.000000000000000000, 1.677772373332757194, -3.535253723897187506 ) ) ;
#12316=PRODUCT_DEFINITION ( 'UNKNOWN', '', #4855, #968 ) ;
#12323=CARTESIAN_POINT ( 'NONE',  ( -2.688821387764050996E-14, -4.618802153517012954, -0.4999999999999995559 ) ) ;
#12328=VECTOR ( 'NONE', #1130, 999.9999999999998863 ) ;
#12335=EDGE_CURVE ( 'NONE', #6584, #5823, #8945, .T. ) ;
#12362=CARTESIAN_POINT ( 'NONE',  ( -3.333333333333332149, -2.694301256218264218, -3.300726591567082036 ) ) ;
#12366=CARTESIAN_POINT ( 'NONE',  ( 4.000000000001088907, 1.658577278524410170, -3.531553309554541720 ) ) ;
#12386=DIRECTION ( 'NONE',  ( 0.000000000000000000, 0.000000000000000000, -1.000000000000000000 ) ) ;
#12407=EDGE_CURVE ( 'NONE', #7344, #1304, #1580, .T. ) ;
#12424=ORIENTED_EDGE ( 'NONE', *, *, #9057, .F. ) ;
#12445=DIRECTION ( 'NONE',  ( 1.000000000000000000, 0.000000000000000000, 0.000000000000000000 ) ) ;
#12451=CARTESIAN_POINT ( 'NONE',  ( -4.203934362469166963, -1.640673743454851286, -3.598432614606932756 ) ) ;
#12478=ORIENTED_EDGE ( 'NONE', *, *, #7115, .T. ) ;
#12480=CARTESIAN_POINT ( 'NONE',  ( 3.333333333333332593, 2.694301256218250007, -3.300726591567078483 ) ) ;
#12482=EDGE_CURVE ( 'NONE', #9288, #7686, #2186, .T. ) ;
#12486=CARTESIAN_POINT ( 'NONE',  ( -3.455068668934486276, 2.624017327439035707, -3.316620875263955437 ) ) ;
#12488=DIRECTION ( 'NONE',  ( -0.000000000000000000, -0.000000000000000000, 1.000000000000000000 ) ) ;
#12491=EDGE_LOOP ( 'NONE', ( #2248, #11589, #10924, #5877 ) ) ;
#12494=ORIENTED_EDGE ( 'NONE', *, *, #12407, .T. ) ;
#12506=DIRECTION ( 'NONE',  ( 0.000000000000000000, 0.000000000000000000, -1.000000000000000000 ) ) ;
#12515=CARTESIAN_POINT ( 'NONE',  ( 4.197393957002303999, 7.772902908466098641E-14, -3.503767560748929810 ) ) ;
#12519=ADVANCED_FACE ( 'NONE', ( #4543 ), #10274, .T. ) ;
#12521=CARTESIAN_POINT ( 'NONE',  ( -4.197477534772231955, 0.8522413273724368521, -3.505042416683225692 ) ) ;
#12522=ADVANCED_FACE ( 'NONE', ( #10630 ), #2534, .T. ) ;
#12541=EDGE_CURVE ( 'NONE', #4606, #8295, #10490, .T. ) ;
#12550=VERTEX_POINT ( 'NONE', #8830 ) ;
#12568=CARTESIAN_POINT ( 'NONE',  ( 0.000000000000000000, 0.000000000000000000, -4.974599999999998801 ) ) ;
#12573=CARTESIAN_POINT ( 'NONE',  ( -2.499999999999999556, 3.061616997868382648E-16, 3.469446951953614189E-15 ) ) ;
#12577=AXIS2_PLACEMENT_3D ( 'NONE', #11328, #13182, #658 ) ;
#12580=AXIS2_PLACEMENT_3D ( 'NONE', #8043, #10038, #13145 ) ;
#12581=EDGE_CURVE ( 'NONE', #13574, #6658, #6232, .T. ) ;
#12591=CARTESIAN_POINT ( 'NONE',  ( 4.000000000000000888, 1.563622288139206118, -0.2253451193528334950 ) ) ;
#12596=AXIS2_PLACEMENT_3D ( 'NONE', #4927, #4854, #9139 ) ;
#12607=CARTESIAN_POINT ( 'NONE',  ( 4.000000000000000000, -2.309401076758514915, -3.433295621305383349 ) ) ;
#12621=ADVANCED_FACE ( 'NONE', ( #13030 ), #9636, .F. ) ;
#12623=CARTESIAN_POINT ( 'NONE',  ( 0.1750025118121568690, 4.719839900820621104, -3.469254087858248070 ) ) ;
#12632=ORIENTED_EDGE ( 'NONE', *, *, #4161, .F. ) ;
#12633=CARTESIAN_POINT ( 'NONE',  ( -2.742827927723112236, -3.035229711105190464, -3.433252694550595230 ) ) ;
#12647=CARTESIAN_POINT ( 'NONE',  ( 0.000000000000000000, 0.000000000000000000, 0.000000000000000000 ) ) ;
#12650=CARTESIAN_POINT ( 'NONE',  ( 0.5636800770130377947, 4.293361309317166530, -3.531542292954102713 ) ) ;
#12660=CARTESIAN_POINT ( 'NONE',  ( -6.259644161404860030E-16, -4.618802153517027165, -3.433295621305388234 ) ) ;
#12669=PLANE ( 'NONE',  #5374 ) ;
#12676=DIRECTION ( 'NONE',  ( -1.000000000000000000, 0.000000000000000000, 0.000000000000000000 ) ) ;
#12683=CARTESIAN_POINT ( 'NONE',  ( -4.000000000000000000, -1.942223658245633811, -0.3516579909967644246 ) ) ;
#12686=CARTESIAN_POINT ( 'NONE',  ( -4.236525694536558362, 2.416953475386465211, -3.751298745799836354 ) ) ;
#12700=CARTESIAN_POINT ( 'NONE',  ( -2.345747346278108214, 3.264484291692489215, -0.01223254789873409049 ) ) ;
#12725=CARTESIAN_POINT ( 'NONE',  ( -2.000000000000007550, -3.464101615137749945, 0.000000000000000000 ) ) ;
#12730=LINE ( 'NONE', #6402, #5745 ) ;
#12732=CARTESIAN_POINT ( 'NONE',  ( 3.999999999999999112, -1.539600717839012978, -3.300726591567080703 ) ) ;
#12748=CARTESIAN_POINT ( 'NONE',  ( 2.059999999999998721, 0.000000000000000000, -0.3080913168122742518 ) ) ;
#12788=ORIENTED_EDGE ( 'NONE', *, *, #6618, .F. ) ;
#12794=DIRECTION ( 'NONE',  ( -0.000000000000000000, -0.000000000000000000, 1.000000000000000000 ) ) ;
#12801=DIRECTION ( 'NONE',  ( -0.8660254037844377084, -0.5000000000000015543, 0.000000000000000000 ) ) ;
#12820=B_SPLINE_CURVE_WITH_KNOTS ( 'NONE', 3,
 ( #12725, #2491, #3333, #4435, #282, #6659 ),
 .UNSPECIFIED., .F., .F.,
 ( 4, 2, 4 ),
 ( 0.002365888236228001588, 0.003551327329835089319, 0.004736766423442177049 ),
 .UNSPECIFIED. ) ;
#12823=UNCERTAINTY_MEASURE_WITH_UNIT (LENGTH_MEASURE( 1.000000000000000082E-05 ), #7576, 'distance_accuracy_value', 'NONE');
#12826=CARTESIAN_POINT ( 'NONE',  ( -1.274258131565027874, -3.883108878240886241, -3.220599429844051009 ) ) ;
#12867=PLANE ( 'NONE',  #7132 ) ;
#12903=CARTESIAN_POINT ( 'NONE',  ( -4.211140560182196957, -2.431303136016552013, -3.745885042887436178 ) ) ;
#12917=EDGE_CURVE ( 'NONE', #7909, #5823, #3154, .T. ) ;
#12934=FACE_OUTER_BOUND ( 'NONE', #9790, .T. ) ;
#12951=CARTESIAN_POINT ( 'NONE',  ( 4.024499207728657879, -2.323545700935587988, -3.572172305156509964 ) ) ;
#12957=CARTESIAN_POINT ( 'NONE',  ( 4.000000000000000000, -2.309401076758516691, -0.4999999999999995559 ) ) ;
#12961=CARTESIAN_POINT ( 'NONE',  ( 4.101954839143060028, 2.368264730582927857, -3.681130640444267854 ) ) ;
#13001=CARTESIAN_POINT ( 'NONE',  ( 4.000000000000000000, 2.309401076758515803, -0.4999999999999995559 ) ) ;
#13013=FACE_OUTER_BOUND ( 'NONE', #2489, .T. ) ;
#13030=FACE_OUTER_BOUND ( 'NONE', #13224, .T. ) ;
#13047=AXIS2_PLACEMENT_3D ( 'NONE', #3545, #3617, #1243 ) ;
#13078=ORIENTED_EDGE ( 'NONE', *, *, #883, .T. ) ;
#13096=CARTESIAN_POINT ( 'NONE',  ( 2.171643655288379993, -3.365003104552334978, -1.195831703456429434E-14 ) ) ;
#13097=DIRECTION ( 'NONE',  ( 0.000000000000000000, -1.000000000000000000, 0.000000000000000000 ) ) ;
#13115=ORIENTED_EDGE ( 'NONE', *, *, #4935, .T. ) ;
#13145=DIRECTION ( 'NONE',  ( -1.000000000000000000, 0.000000000000000000, 0.000000000000000000 ) ) ;
#13156=CARTESIAN_POINT ( 'NONE',  ( 0.000000000000000000, 0.000000000000000000, 0.000000000000000000 ) ) ;
#13157=B_SPLINE_CURVE_WITH_KNOTS ( 'NONE', 3,
 ( #5830, #11133, #9210, #1653, #8105 ),
 .UNSPECIFIED., .F., .F.,
 ( 4, 1, 4 ),
 ( 5.640274452250024914E-20, 0.002309401076758505356, 0.004618802153517010713 ),
 .UNSPECIFIED. ) ;
#13162=DIRECTION ( 'NONE',  ( 0.000000000000000000, 0.000000000000000000, -1.000000000000000000 ) ) ;
#13182=DIRECTION ( 'NONE',  ( -0.000000000000000000, -0.000000000000000000, 1.000000000000000000 ) ) ;
#13189=ORIENTED_EDGE ( 'NONE', *, *, #11334, .T. ) ;
#13191=ORIENTED_EDGE ( 'NONE', *, *, #3665, .F. ) ;
#13202=( GEOMETRIC_REPRESENTATION_CONTEXT ( 3 ) GLOBAL_UNCERTAINTY_ASSIGNED_CONTEXT ( ( #1472 ) ) GLOBAL_UNIT_ASSIGNED_CONTEXT ( ( #7653, #9722, #1397 ) ) REPRESENTATION_CONTEXT ( 'NONE', 'WORKASPACE' ) );
#13217=FACE_OUTER_BOUND ( 'NONE', #923, .T. ) ;
#13224=EDGE_LOOP ( 'NONE', ( #13589, #2925, #9116, #2002 ) ) ;
#13227=CARTESIAN_POINT ( 'NONE',  ( 2.000000000000005329, -3.464101615137751722, 0.000000000000000000 ) ) ;
#13306=DIRECTION ( 'NONE',  ( 0.000000000000000000, 0.000000000000000000, 1.000000000000000000 ) ) ;
#13317=CARTESIAN_POINT ( 'NONE',  ( 4.000000000000000000, 0.8378280264232961239, -3.220590601395640018 ) ) ;
#13329=CARTESIAN_POINT ( 'NONE',  ( -2.804994570502171047, -3.229033611042465335, -3.526374918436838701 ) ) ;
#13343=AXIS2_PLACEMENT_3D ( 'NONE', #122, #4343, #8559 ) ;
#13344=CARTESIAN_POINT ( 'NONE',  ( 1.654252653721905331, 3.663718938583014229, -0.01223254789873410957 ) ) ;
#13389=CARTESIAN_POINT ( 'NONE',  ( -4.207491450040567571, 2.029819825146470524, -3.671670828759566074 ) ) ;
#13399=DIRECTION ( 'NONE',  ( 0.000000000000000000, 0.000000000000000000, -1.000000000000000000 ) ) ;
#13405=CARTESIAN_POINT ( 'NONE',  ( -4.000000000000000000, -0.8382240730041925492, -3.220610619767135141 ) ) ;
#13411=VERTEX_POINT ( 'NONE', #10108 ) ;
#13424=CARTESIAN_POINT ( 'NONE',  ( -4.000000000000000000, 2.309401076758498483, -3.433295621305379353 ) ) ;
#13438=CARTESIAN_POINT ( 'NONE',  ( -2.725741868435985094, 3.045094352034055429, -3.220599429844047012 ) ) ;
#13459=AXIS2_PLACEMENT_3D ( 'NONE', #7512, #11785, #2216 ) ;
#13467=CYLINDRICAL_SURFACE ( 'NONE', #4465, 2.100000000000000089 ) ;
#13470=CARTESIAN_POINT ( 'NONE',  ( 2.756197834950227410, 3.027510591568626896, -3.223146290109805356 ) ) ;
#13475=B_SPLINE_CURVE_WITH_KNOTS ( 'NONE', 3,
 ( #12660, #10390, #11361, #3200, #2147, #900 ),
 .UNSPECIFIED., .F., .F.,
 ( 4, 2, 4 ),
 ( 0.000000000000000000, 0.0002095117440854740156, 0.0004190234881709480313 ),
 .UNSPECIFIED. ) ;
#13478=PRODUCT ( 'hex flange nut gradea_iso_ISO - 4161 - M5 - N', 'hex flange nut gradea_iso_ISO - 4161 - M5 - N', '', ( #6061 ) ) ;
#13491=AXIS2_PLACEMENT_3D ( 'NONE', #3493, #5450, #2514 ) ;
#13503=ORIENTED_EDGE ( 'NONE', *, *, #11221, .F. ) ;
#13514=AXIS2_PLACEMENT_3D ( 'NONE', #8110, #12386, #2848 ) ;
#13533=CARTESIAN_POINT ( 'NONE',  ( 2.499999999999999556, 0.000000000000000000, 3.469446951953614189E-15 ) ) ;
#13534=CARTESIAN_POINT ( 'NONE',  ( -4.211140560182196957, -2.431303136016552013, -3.745885042887436178 ) ) ;
#13538=ORIENTED_EDGE ( 'NONE', *, *, #12917, .F. ) ;
#13542=DIRECTION ( 'NONE',  ( 0.000000000000000000, 0.000000000000000000, 1.000000000000000000 ) ) ;
#13544=CARTESIAN_POINT ( 'NONE',  ( 3.540020015735602765, 2.810662092924382627, -3.602146406945867962 ) ) ;
#13549=CARTESIAN_POINT ( 'NONE',  ( 4.000000000000000000, 0.9868501483902631932, -0.09357334158579604100 ) ) ;
#13567=DIRECTION ( 'NONE',  ( 0.8191520442889902442, 1.003171929053522651E-16, -0.5735764363510482688 ) ) ;
#13570=CARTESIAN_POINT ( 'NONE',  ( -4.211140560182196957, 2.431303136016537803, -3.745885042887433514 ) ) ;
#13574=VERTEX_POINT ( 'NONE', #10664 ) ;
#13578=CARTESIAN_POINT ( 'NONE',  ( 0.6666666666666689611, 4.233901974057261874, -3.300726591567082480 ) ) ;
#13583=FACE_OUTER_BOUND ( 'NONE', #7537, .T. ) ;
#13586=CARTESIAN_POINT ( 'NONE',  ( 3.999999999999999112, -0.7890432684750902093, -0.04868663549882291247 ) ) ;
#13589=ORIENTED_EDGE ( 'NONE', *, *, #99, .T. ) ;
#13617=CARTESIAN_POINT ( 'NONE',  ( -4.211399284164270895, 2.459729995988205964, -3.751162237960538715 ) ) ;
#13620=ORIENTED_EDGE ( 'NONE', *, *, #2118, .T. ) ;
#13623=CARTESIAN_POINT ( 'NONE',  ( 5.384454397937118664, 0.000000000000000000, -5.000000000000000000 ) ) ;
#13706=COLOUR_RGB('Black',0.12,0.14,0.17);
#13707=FILL_AREA_STYLE_COLOUR('',#13706);
#13708=FILL_AREA_STYLE('',(#13707));
#13709=SURFACE_STYLE_FILL_AREA(#13708);
#13710=SURFACE_SIDE_STYLE('',(#13709));
#13711=SURFACE_STYLE_USAGE(.BOTH.,#13710);
#13712=PRESENTATION_STYLE_ASSIGNMENT((#13711));
ENDSEC;
END-ISO-10303-21;
